ISO-10303-21;
HEADER;
/* Generated by software containing ST-Developer
 * from STEP Tools, Inc. (www.steptools.com) 
 */

FILE_DESCRIPTION(
/* description */ (''),
/* implementation_level */ '2;1');

FILE_NAME(
/* name */ 'Hex nut M3.step',
/* time_stamp */ '2026-11-10T09:09:39-08:00',
/* author */ (''),
/* organization */ (''),
/* preprocessor_version */ 'ST-DEVELOPER v20.2',
/* originating_system */ 'Autodesk Translation Framework v15.17.0.0',
/* authorisation */ '');

FILE_SCHEMA (('AUTOMOTIVE_DESIGN { 1 0 10303 214 3 1 1 }'));
ENDSEC;

DATA;
#10=MECHANICAL_DESIGN_GEOMETRIC_PRESENTATION_REPRESENTATION('',(#562),#18353);
#169=B_SPLINE_SURFACE_WITH_KNOTS('',3,3,((#17726,#17727,#17728,#17729,#17730,
#17731,#17732,#17733,#17734,#17735,#17736,#17737,#17738,#17739,#17740,#17741,
#17742,#17743,#17744,#17745,#17746,#17747,#17748,#17749,#17750,#17751,#17752,
#17753,#17754,#17755,#17756,#17757,#17758,#17759,#17760,#17761),(#17762,
#17763,#17764,#17765,#17766,#17767,#17768,#17769,#17770,#17771,#17772,#17773,
#17774,#17775,#17776,#17777,#17778,#17779,#17780,#17781,#17782,#17783,#17784,
#17785,#17786,#17787,#17788,#17789,#17790,#17791,#17792,#17793,#17794,#17795,
#17796,#17797),(#17798,#17799,#17800,#17801,#17802,#17803,#17804,#17805,
#17806,#17807,#17808,#17809,#17810,#17811,#17812,#17813,#17814,#17815,#17816,
#17817,#17818,#17819,#17820,#17821,#17822,#17823,#17824,#17825,#17826,#17827,
#17828,#17829,#17830,#17831,#17832,#17833),(#17834,#17835,#17836,#17837,
#17838,#17839,#17840,#17841,#17842,#17843,#17844,#17845,#17846,#17847,#17848,
#17849,#17850,#17851,#17852,#17853,#17854,#17855,#17856,#17857,#17858,#17859,
#17860,#17861,#17862,#17863,#17864,#17865,#17866,#17867,#17868,#17869)),
 .UNSPECIFIED.,.F.,.F.,.F.,(4,4),(4,1,1,1,1,1,1,1,1,1,1,1,1,1,1,1,1,1,1,
1,1,1,1,1,1,1,1,1,1,1,1,1,1,4),(0.,0.0321584099938622),(11.8553612635794,
12.830508595889,13.8056559281987,14.7808032605084,15.755950592818,16.7310979251277,
17.7062452574374,18.681392589747,19.6565399220567,20.6316872543664,21.606834586676,
22.5819819189857,23.5571292512954,24.532276583605,25.5074239159147,26.4825712482243,
27.457718580534,28.4328659128437,29.4080132451533,30.383160577463,31.3583079097727,
32.3334552420823,33.308602574392,34.2837499067017,35.2588972390113,36.234044571321,
37.2091919036307,38.1843392359403,39.15948656825,40.1346339005596,41.1097812328693,
42.084928565179,43.0600758974886,44.0352232297983),.UNSPECIFIED.);
#170=B_SPLINE_SURFACE_WITH_KNOTS('',3,3,((#17993,#17994,#17995,#17996,#17997,
#17998,#17999,#18000,#18001,#18002,#18003,#18004,#18005,#18006,#18007,#18008,
#18009,#18010,#18011,#18012,#18013,#18014,#18015,#18016,#18017,#18018,#18019,
#18020,#18021,#18022,#18023,#18024,#18025,#18026,#18027,#18028),(#18029,
#18030,#18031,#18032,#18033,#18034,#18035,#18036,#18037,#18038,#18039,#18040,
#18041,#18042,#18043,#18044,#18045,#18046,#18047,#18048,#18049,#18050,#18051,
#18052,#18053,#18054,#18055,#18056,#18057,#18058,#18059,#18060,#18061,#18062,
#18063,#18064),(#18065,#18066,#18067,#18068,#18069,#18070,#18071,#18072,
#18073,#18074,#18075,#18076,#18077,#18078,#18079,#18080,#18081,#18082,#18083,
#18084,#18085,#18086,#18087,#18088,#18089,#18090,#18091,#18092,#18093,#18094,
#18095,#18096,#18097,#18098,#18099,#18100),(#18101,#18102,#18103,#18104,
#18105,#18106,#18107,#18108,#18109,#18110,#18111,#18112,#18113,#18114,#18115,
#18116,#18117,#18118,#18119,#18120,#18121,#18122,#18123,#18124,#18125,#18126,
#18127,#18128,#18129,#18130,#18131,#18132,#18133,#18134,#18135,#18136)),
 .UNSPECIFIED.,.F.,.F.,.F.,(4,4),(4,1,1,1,1,1,1,1,1,1,1,1,1,1,1,1,1,1,1,
1,1,1,1,1,1,1,1,1,1,1,1,1,1,4),(0.,0.0321584099938622),(14.3984001269719,
15.3735474592815,16.3486947915912,17.3238421239009,18.2989894562105,19.2741367885202,
20.2492841208299,21.2244314531395,22.1995787854492,23.1747261177589,24.1498734500685,
25.1250207823782,26.1001681146879,27.0753154469975,28.0504627793072,29.0256101116168,
30.0007574439265,30.9759047762362,31.9510521085458,32.9261994408555,33.9013467731652,
34.8764941054748,35.8516414377845,36.8267887700942,37.8019361024038,38.7770834347135,
39.7522307670232,40.7273780993328,41.7025254316425,42.6776727639522,43.6528200962618,
44.6279674285715,45.6031147608811,46.5782620931908),.UNSPECIFIED.);
#510=B_SPLINE_CURVE_WITH_KNOTS('',3,(#17396,#17397,#17398,#17399,#17400,
#17401,#17402),.UNSPECIFIED.,.F.,.F.,(4,3,4),(-30.159289474462,-29.2544199692899,
-28.9853432330879),.UNSPECIFIED.);
#511=B_SPLINE_CURVE_WITH_KNOTS('',3,(#17408,#17409,#17410,#17411,#17412,
#17413,#17414,#17415,#17416,#17417,#17418,#17419,#17420,#17421,#17422,#17423,
#17424,#17425,#17426),.UNSPECIFIED.,.F.,.F.,(4,3,3,3,3,3,4),(26.4423043696954,
27.3041253046706,28.2792726369803,29.25441996929,30.2295673015996,31.2047146339093,
32.179861966219),.UNSPECIFIED.);
#512=B_SPLINE_CURVE_WITH_KNOTS('',3,(#17428,#17429,#17430,#17431,#17432,
#17433,#17434,#17435,#17436,#17437,#17438,#17439,#17440,#17441,#17442,#17443,
#17444,#17445,#17446,#17447,#17448,#17449),.UNSPECIFIED.,.F.,.F.,(4,3,3,
3,3,3,3,4),(-28.9853432330879,-28.2792726369803,-27.3041253046706,-26.3289779723609,
-25.3538306400513,-24.3786833077416,-23.403535975432,-22.7021579259084),
 .UNSPECIFIED.);
#513=B_SPLINE_CURVE_WITH_KNOTS('',3,(#17454,#17455,#17456,#17457,#17458,
#17459,#17460,#17461,#17462,#17463,#17464,#17465,#17466,#17467,#17468,#17469,
#17470,#17471,#17472,#17473,#17474,#17475,#17476,#17477,#17478),
 .UNSPECIFIED.,.F.,.F.,(4,3,3,3,3,3,3,3,4),(20.1591190625159,20.478093978503,
21.4532413108126,22.4283886431223,23.403535975432,24.3786833077416,25.3538306400513,
26.328977972361,26.4423043696954),.UNSPECIFIED.);
#514=B_SPLINE_CURVE_WITH_KNOTS('',3,(#17479,#17480,#17481,#17482,#17483,
#17484,#17485,#17486,#17487,#17488,#17489,#17490,#17491,#17492,#17493,#17494,
#17495,#17496,#17497,#17498,#17499,#17500,#17501,#17502,#17503),
 .UNSPECIFIED.,.F.,.F.,(4,3,3,3,3,3,3,3,4),(-22.7021579259084,-22.4283886431223,
-21.4532413108126,-20.478093978503,-19.5029466461933,-18.5277993138836,
-17.552651981574,-16.5775046492643,-16.4189726187288),.UNSPECIFIED.);
#515=B_SPLINE_CURVE_WITH_KNOTS('',3,(#17508,#17509,#17510,#17511,#17512,
#17513,#17514,#17515,#17516,#17517,#17518,#17519,#17520,#17521,#17522,#17523,
#17524,#17525,#17526,#17527,#17528,#17529),.UNSPECIFIED.,.F.,.F.,(4,3,3,
3,3,3,3,4),(13.8759337553363,14.627209984645,15.6023573169546,16.5775046492643,
17.552651981574,18.5277993138836,19.5029466461933,20.1591190625159),
 .UNSPECIFIED.);
#516=B_SPLINE_CURVE_WITH_KNOTS('',3,(#17530,#17531,#17532,#17533,#17534,
#17535,#17536,#17537,#17538,#17539,#17540,#17541,#17542,#17543,#17544,#17545,
#17546,#17547,#17548,#17549,#17550,#17551),.UNSPECIFIED.,.F.,.F.,(4,3,3,
3,3,3,3,4),(-16.4189726187288,-15.6023573169546,-14.627209984645,-13.6520626523353,
-12.6769153200256,-11.701767987716,-10.7266206554063,-10.1357873115492),
 .UNSPECIFIED.);
#517=B_SPLINE_CURVE_WITH_KNOTS('',3,(#17557,#17558,#17559,#17560,#17561,
#17562,#17563,#17564,#17565,#17566,#17567,#17568,#17569),.UNSPECIFIED.,
 .F.,.F.,(4,3,3,3,4),(-3.8526020043696,-2.92544199692899,-1.95029466461933,
-0.975147332309664,0.),.UNSPECIFIED.);
#518=B_SPLINE_CURVE_WITH_KNOTS('',3,(#17572,#17573,#17574,#17575,#17576,
#17577,#17578,#17579,#17580,#17581,#17582,#17583,#17584,#17585,#17586,#17587,
#17588,#17589,#17590),.UNSPECIFIED.,.F.,.F.,(4,3,3,3,3,3,4),(2.02057249175693,
2.925441996929,3.90058932923866,4.87573666154832,5.85088399385799,6.82603132616766,
7.59274844815668),.UNSPECIFIED.);
#519=B_SPLINE_CURVE_WITH_KNOTS('',3,(#17596,#17597,#17598,#17599,#17600,
#17601,#17602),.UNSPECIFIED.,.F.,.F.,(4,1,1,1,4),(40.8407044966673,41.1097812328693,
42.084928565179,43.0600758974886,44.0352232297983),.UNSPECIFIED.);
#520=B_SPLINE_CURVE_WITH_KNOTS('',3,(#17605,#17606,#17607,#17608,#17609,
#17610,#17611),.UNSPECIFIED.,.F.,.F.,(4,1,1,1,4),(40.8407044966673,41.7025254316425,
42.6776727639522,43.6528200962618,44.5576896014339),.UNSPECIFIED.);
#521=B_SPLINE_CURVE_WITH_KNOTS('',3,(#17616,#17617,#17618,#17619,#17620,
#17621,#17622,#17623,#17624,#17625),.UNSPECIFIED.,.F.,.F.,(4,1,1,1,1,1,
1,4),(34.5575191894877,35.2588972390113,36.234044571321,37.2091919036307,
38.1843392359403,39.15948656825,40.1346339005596,40.8407044966673),
 .UNSPECIFIED.);
#522=B_SPLINE_CURVE_WITH_KNOTS('',3,(#17626,#17627,#17628,#17629,#17630,
#17631,#17632,#17633,#17634,#17635,#17636),.UNSPECIFIED.,.F.,.F.,(4,1,1,
1,1,1,1,1,4),(34.5575191894877,34.8764941054748,35.8516414377845,36.8267887700942,
37.8019361024038,38.7770834347135,39.7522307670232,40.7273780993328,40.8407044966673),
 .UNSPECIFIED.);
#523=B_SPLINE_CURVE_WITH_KNOTS('',3,(#17641,#17642,#17643,#17644,#17645,
#17646,#17647,#17648,#17649,#17650,#17651),.UNSPECIFIED.,.F.,.F.,(4,1,1,
1,1,1,1,1,4),(28.2743338823081,28.4328659128437,29.4080132451533,30.383160577463,
31.3583079097727,32.3334552420823,33.308602574392,34.2837499067017,34.5575191894877),
 .UNSPECIFIED.);
#524=B_SPLINE_CURVE_WITH_KNOTS('',3,(#17652,#17653,#17654,#17655,#17656,
#17657,#17658,#17659,#17660,#17661),.UNSPECIFIED.,.F.,.F.,(4,1,1,1,1,1,
1,4),(28.2743338823081,29.0256101116168,30.0007574439265,30.9759047762362,
31.9510521085458,32.9261994408555,33.9013467731652,34.5575191894877),
 .UNSPECIFIED.);
#525=B_SPLINE_CURVE_WITH_KNOTS('',3,(#17666,#17667,#17668,#17669,#17670,
#17671,#17672,#17673,#17674,#17675),.UNSPECIFIED.,.F.,.F.,(4,1,1,1,1,1,
1,4),(21.9911485751285,22.5819819189857,23.5571292512954,24.532276583605,
25.5074239159147,26.4825712482243,27.457718580534,28.2743338823081),
 .UNSPECIFIED.);
#526=B_SPLINE_CURVE_WITH_KNOTS('',3,(#17676,#17677,#17678,#17679,#17680,
#17681,#17682,#17683,#17684,#17685,#17686),.UNSPECIFIED.,.F.,.F.,(4,1,1,
1,1,1,1,1,4),(21.9911485751285,22.1995787854492,23.1747261177589,24.1498734500685,
25.1250207823782,26.1001681146879,27.0753154469975,28.0504627793072,28.2743338823081),
 .UNSPECIFIED.);
#527=B_SPLINE_CURVE_WITH_KNOTS('',3,(#17692,#17693,#17694,#17695,#17696),
 .UNSPECIFIED.,.F.,.F.,(4,1,4),(14.3984001269719,15.3735474592815,15.7079632679489),
 .UNSPECIFIED.);
#528=B_SPLINE_CURVE_WITH_KNOTS('',3,(#17699,#17700,#17701,#17702,#17703),
 .UNSPECIFIED.,.F.,.F.,(4,1,4),(13.8759337553363,14.7808032605084,15.7079632679489),
 .UNSPECIFIED.);
#529=B_SPLINE_CURVE_WITH_KNOTS('',3,(#17705,#17706,#17707,#17708,#17709,
#17710,#17711,#17712,#17713,#17714,#17715),.UNSPECIFIED.,.F.,.F.,(4,1,1,
1,1,1,1,1,4),(15.7079632679489,15.755950592818,16.7310979251277,17.7062452574374,
18.681392589747,19.6565399220567,20.6316872543664,21.606834586676,21.9911485751285),
 .UNSPECIFIED.);
#530=B_SPLINE_CURVE_WITH_KNOTS('',3,(#17716,#17717,#17718,#17719,#17720,
#17721,#17722,#17723,#17724,#17725),.UNSPECIFIED.,.F.,.F.,(4,1,1,1,1,1,
1,4),(15.7079632679489,16.3486947915912,17.3238421239009,18.2989894562105,
19.2741367885202,20.2492841208299,21.2244314531395,21.9911485751285),
 .UNSPECIFIED.);
#531=B_SPLINE_CURVE_WITH_KNOTS('',3,(#17870,#17871,#17872,#17873,#17874,
#17875,#17876,#17877,#17878,#17879,#17880,#17881,#17882,#17883,#17884,#17885,
#17886,#17887,#17888,#17889,#17890,#17891,#17892,#17893,#17894,#17895,#17896,
#17897,#17898,#17899,#17900,#17901,#17902,#17903,#17904,#17905,#17906,#17907,
#17908,#17909,#17910,#17911,#17912,#17913,#17914,#17915,#17916,#17917,#17918),
 .UNSPECIFIED.,.F.,.F.,(4,3,3,3,3,3,3,3,3,3,3,3,3,3,3,3,4),(0.,0.0320333804888866,
0.0505515708593653,0.0603413132804416,0.0917900141854983,0.108096115778005,
0.122914675479851,0.145143248337739,0.168151513577436,0.177516949333476,
0.202471322707608,0.21794283081622,0.231200110368267,0.247503117401854,
0.263651632124391,0.277334442830003,0.286347380332244),.UNSPECIFIED.);
#532=B_SPLINE_CURVE_WITH_KNOTS('',3,(#17919,#17920,#17921,#17922,#17923,
#17924,#17925,#17926,#17927,#17928,#17929,#17930,#17931,#17932,#17933,#17934,
#17935,#17936,#17937,#17938,#17939,#17940,#17941,#17942,#17943,#17944,#17945,
#17946,#17947,#17948,#17949,#17950,#17951,#17952,#17953,#17954,#17955,#17956,
#17957,#17958,#17959,#17960,#17961,#17962,#17963,#17964,#17965,#17966,#17967),
 .UNSPECIFIED.,.F.,.F.,(4,3,3,3,3,3,3,3,3,3,3,3,3,3,3,3,4),(0.,0.0274305464075637,
0.0492901149097146,0.0591933555873536,0.0887250095166089,0.100015570674795,
0.108381796308415,0.130826479038955,0.152531076563578,0.162815893631175,
0.190691958353668,0.212372986031639,0.222945305605857,0.245534254906135,
0.257847836118801,0.274320152521146,0.28514280399515),.UNSPECIFIED.);
#533=B_SPLINE_CURVE_WITH_KNOTS('',3,(#17968,#17969,#17970,#17971,#17972,
#17973,#17974,#17975,#17976,#17977,#17978,#17979,#17980,#17981,#17982,#17983,
#17984,#17985,#17986,#17987,#17988,#17989,#17990,#17991,#17992),
 .UNSPECIFIED.,.F.,.F.,(4,3,3,3,3,3,3,3,4),(-10.1357873115492,-9.75147332309665,
-8.77632599078699,-7.80117865847732,-6.82603132616766,-5.85088399385799,
-4.87573666154833,-3.90058932923866,-3.8526020043696),.UNSPECIFIED.);
#534=B_SPLINE_CURVE_WITH_KNOTS('',3,(#18137,#18138,#18139,#18140,#18141,
#18142,#18143,#18144,#18145,#18146,#18147,#18148,#18149,#18150,#18151,#18152,
#18153,#18154,#18155,#18156,#18157,#18158,#18159,#18160,#18161,#18162,#18163,
#18164,#18165,#18166,#18167,#18168,#18169,#18170,#18171,#18172,#18173,#18174,
#18175,#18176,#18177,#18178,#18179,#18180,#18181,#18182,#18183,#18184,#18185),
 .UNSPECIFIED.,.F.,.F.,(4,3,3,3,3,3,3,3,3,3,3,3,3,3,3,3,4),(0.,0.0274305890506951,
0.0492901290331875,0.0591933603491513,0.0887250177779717,0.100015607166709,
0.108381835831352,0.13082647903896,0.152531071764912,0.162815892251191,
0.190691957318683,0.212372984486691,0.22294529735758,0.245534140364172,
0.257847701250626,0.274320152521159,0.285142803995162),.UNSPECIFIED.);
#535=B_SPLINE_CURVE_WITH_KNOTS('',3,(#18186,#18187,#18188,#18189,#18190,
#18191,#18192,#18193,#18194,#18195,#18196,#18197,#18198,#18199,#18200,#18201,
#18202,#18203,#18204,#18205,#18206,#18207,#18208,#18209,#18210),
 .UNSPECIFIED.,.F.,.F.,(4,3,3,3,3,3,3,3,4),(7.59274844815668,7.80117865847732,
8.77632599078698,9.75147332309665,10.7266206554063,11.701767987716,12.6769153200256,
13.6520626523353,13.8759337553363),.UNSPECIFIED.);
#536=B_SPLINE_CURVE_WITH_KNOTS('',3,(#18211,#18212,#18213,#18214,#18215,
#18216,#18217,#18218,#18219,#18220,#18221,#18222,#18223,#18224,#18225,#18226,
#18227,#18228,#18229,#18230,#18231,#18232,#18233,#18234,#18235,#18236,#18237,
#18238,#18239,#18240,#18241,#18242,#18243,#18244,#18245,#18246,#18247,#18248,
#18249,#18250,#18251,#18252,#18253,#18254,#18255,#18256,#18257,#18258,#18259),
 .UNSPECIFIED.,.F.,.F.,(4,3,3,3,3,3,3,3,3,3,3,3,3,3,3,3,4),(0.,0.0320334058164849,
0.0505515938322513,0.0603413311462071,0.0917900214840119,0.108096111687201,
0.122914678304232,0.145143248337743,0.168151527562726,0.177516955081398,
0.202471327018552,0.217942288122009,0.231200024743484,0.24750284136614,
0.263651600306541,0.277334442830014,0.286347380332252),.UNSPECIFIED.);
#544=SHAPE_REPRESENTATION_RELATIONSHIP('SRR','None',#18405,#553);
#553=ADVANCED_BREP_SHAPE_REPRESENTATION('',(#571),#18351);
#562=STYLED_ITEM('',(#18461),#571);
#571=MANIFOLD_SOLID_BREP('Body1',#6493);
#634=FACE_BOUND('',#1575,.T.);
#635=FACE_BOUND('',#1584,.T.);
#772=PLANE('',#7048);
#773=PLANE('',#7050);
#774=PLANE('',#7051);
#775=PLANE('',#7052);
#776=PLANE('',#7053);
#777=PLANE('',#7054);
#778=PLANE('',#7055);
#779=PLANE('',#7056);
#1129=FACE_OUTER_BOUND('',#1561,.T.);
#1130=FACE_OUTER_BOUND('',#1562,.T.);
#1131=FACE_OUTER_BOUND('',#1563,.T.);
#1132=FACE_OUTER_BOUND('',#1564,.T.);
#1133=FACE_OUTER_BOUND('',#1565,.T.);
#1134=FACE_OUTER_BOUND('',#1566,.T.);
#1135=FACE_OUTER_BOUND('',#1567,.T.);
#1136=FACE_OUTER_BOUND('',#1568,.T.);
#1137=FACE_OUTER_BOUND('',#1569,.T.);
#1138=FACE_OUTER_BOUND('',#1570,.T.);
#1139=FACE_OUTER_BOUND('',#1571,.T.);
#1140=FACE_OUTER_BOUND('',#1572,.T.);
#1141=FACE_OUTER_BOUND('',#1573,.T.);
#1142=FACE_OUTER_BOUND('',#1574,.T.);
#1143=FACE_OUTER_BOUND('',#1576,.T.);
#1144=FACE_OUTER_BOUND('',#1577,.T.);
#1145=FACE_OUTER_BOUND('',#1578,.T.);
#1146=FACE_OUTER_BOUND('',#1579,.T.);
#1147=FACE_OUTER_BOUND('',#1580,.T.);
#1148=FACE_OUTER_BOUND('',#1581,.T.);
#1149=FACE_OUTER_BOUND('',#1582,.T.);
#1150=FACE_OUTER_BOUND('',#1583,.T.);
#1561=EDGE_LOOP('',(#5850,#5851,#5852));
#1562=EDGE_LOOP('',(#5853,#5854,#5855,#5856,#5857));
#1563=EDGE_LOOP('',(#5858,#5859,#5860,#5861));
#1564=EDGE_LOOP('',(#5862,#5863,#5864,#5865));
#1565=EDGE_LOOP('',(#5866,#5867,#5868,#5869));
#1566=EDGE_LOOP('',(#5870,#5871,#5872,#5873));
#1567=EDGE_LOOP('',(#5874,#5875,#5876,#5877));
#1568=EDGE_LOOP('',(#5878,#5879,#5880,#5881));
#1569=EDGE_LOOP('',(#5882,#5883,#5884,#5885));
#1570=EDGE_LOOP('',(#5886,#5887,#5888,#5889));
#1571=EDGE_LOOP('',(#5890,#5891,#5892,#5893));
#1572=EDGE_LOOP('',(#5894,#5895,#5896,#5897,#5898,#5899,#5900,#5901,#5902,
#5903,#5904,#5905,#5906,#5907));
#1573=EDGE_LOOP('',(#5908,#5909,#5910,#5911,#5912,#5913,#5914,#5915,#5916,
#5917,#5918,#5919,#5920));
#1574=EDGE_LOOP('',(#5921,#5922,#5923,#5924,#5925,#5926));
#1575=EDGE_LOOP('',(#5927,#5928,#5929,#5930));
#1576=EDGE_LOOP('',(#5931,#5932,#5933,#5934));
#1577=EDGE_LOOP('',(#5935,#5936,#5937,#5938));
#1578=EDGE_LOOP('',(#5939,#5940,#5941,#5942));
#1579=EDGE_LOOP('',(#5943,#5944,#5945,#5946));
#1580=EDGE_LOOP('',(#5947,#5948,#5949,#5950));
#1581=EDGE_LOOP('',(#5951,#5952,#5953,#5954));
#1582=EDGE_LOOP('',(#5955,#5956,#5957,#5958));
#1583=EDGE_LOOP('',(#5959,#5960,#5961,#5962,#5963,#5964));
#1584=EDGE_LOOP('',(#5965,#5966,#5967,#5968,#5969));
#1965=LINE('',#17393,#2369);
#1966=LINE('',#17406,#2370);
#1967=LINE('',#17453,#2371);
#1968=LINE('',#17507,#2372);
#1969=LINE('',#17555,#2373);
#1970=LINE('',#17594,#2374);
#1971=LINE('',#17615,#2375);
#1972=LINE('',#17640,#2376);
#1973=LINE('',#17665,#2377);
#1974=LINE('',#17690,#2378);
#1975=LINE('',#18263,#2379);
#1976=LINE('',#18265,#2380);
#1977=LINE('',#18267,#2381);
#1978=LINE('',#18269,#2382);
#1979=LINE('',#18271,#2383);
#1980=LINE('',#18272,#2384);
#1981=LINE('',#18277,#2385);
#1982=LINE('',#18278,#2386);
#1983=LINE('',#18279,#2387);
#1984=LINE('',#18282,#2388);
#1985=LINE('',#18283,#2389);
#1986=LINE('',#18286,#2390);
#1987=LINE('',#18287,#2391);
#1988=LINE('',#18290,#2392);
#1989=LINE('',#18291,#2393);
#1990=LINE('',#18294,#2394);
#1991=LINE('',#18295,#2395);
#1992=LINE('',#18297,#2396);
#2369=VECTOR('',#8332,0.15);
#2370=VECTOR('',#8337,0.15);
#2371=VECTOR('',#8342,0.15);
#2372=VECTOR('',#8345,0.15);
#2373=VECTOR('',#8348,0.15);
#2374=VECTOR('',#8353,0.1543);
#2375=VECTOR('',#8358,0.1543);
#2376=VECTOR('',#8361,0.1543);
#2377=VECTOR('',#8364,0.1543);
#2378=VECTOR('',#8367,0.1543);
#2379=VECTOR('',#8374,1.);
#2380=VECTOR('',#8375,1.);
#2381=VECTOR('',#8376,1.);
#2382=VECTOR('',#8377,1.);
#2383=VECTOR('',#8378,1.);
#2384=VECTOR('',#8379,1.);
#2385=VECTOR('',#8384,1.);
#2386=VECTOR('',#8385,1.);
#2387=VECTOR('',#8386,1.);
#2388=VECTOR('',#8389,1.);
#2389=VECTOR('',#8390,1.);
#2390=VECTOR('',#8393,1.);
#2391=VECTOR('',#8394,1.);
#2392=VECTOR('',#8397,1.);
#2393=VECTOR('',#8398,1.);
#2394=VECTOR('',#8401,1.);
#2395=VECTOR('',#8402,1.);
#2396=VECTOR('',#8405,1.);
#2557=CIRCLE('',#7033,0.12645);
#2558=CIRCLE('',#7035,0.12645);
#2559=CIRCLE('',#7039,0.12645);
#2560=CIRCLE('',#7041,0.1543);
#2561=CIRCLE('',#7046,0.1543);
#3127=VERTEX_POINT('',#17391);
#3128=VERTEX_POINT('',#17392);
#3129=VERTEX_POINT('',#17394);
#3130=VERTEX_POINT('',#17404);
#3131=VERTEX_POINT('',#17405);
#3132=VERTEX_POINT('',#17407);
#3133=VERTEX_POINT('',#17451);
#3134=VERTEX_POINT('',#17452);
#3135=VERTEX_POINT('',#17505);
#3136=VERTEX_POINT('',#17506);
#3137=VERTEX_POINT('',#17553);
#3138=VERTEX_POINT('',#17554);
#3139=VERTEX_POINT('',#17556);
#3140=VERTEX_POINT('',#17570);
#3141=VERTEX_POINT('',#17592);
#3142=VERTEX_POINT('',#17593);
#3143=VERTEX_POINT('',#17595);
#3144=VERTEX_POINT('',#17603);
#3145=VERTEX_POINT('',#17613);
#3146=VERTEX_POINT('',#17614);
#3147=VERTEX_POINT('',#17638);
#3148=VERTEX_POINT('',#17639);
#3149=VERTEX_POINT('',#17663);
#3150=VERTEX_POINT('',#17664);
#3151=VERTEX_POINT('',#17688);
#3152=VERTEX_POINT('',#17689);
#3153=VERTEX_POINT('',#17691);
#3154=VERTEX_POINT('',#17697);
#3155=VERTEX_POINT('',#18261);
#3156=VERTEX_POINT('',#18262);
#3157=VERTEX_POINT('',#18264);
#3158=VERTEX_POINT('',#18266);
#3159=VERTEX_POINT('',#18268);
#3160=VERTEX_POINT('',#18270);
#3161=VERTEX_POINT('',#18275);
#3162=VERTEX_POINT('',#18276);
#3163=VERTEX_POINT('',#18281);
#3164=VERTEX_POINT('',#18285);
#3165=VERTEX_POINT('',#18289);
#3166=VERTEX_POINT('',#18293);
#4042=EDGE_CURVE('',#3127,#3128,#1965,.T.);
#4043=EDGE_CURVE('',#3129,#3128,#2557,.F.);
#4044=EDGE_CURVE('',#3129,#3127,#510,.T.);
#4045=EDGE_CURVE('',#3130,#3131,#1966,.T.);
#4046=EDGE_CURVE('',#3131,#3132,#511,.T.);
#4047=EDGE_CURVE('',#3128,#3132,#2558,.F.);
#4048=EDGE_CURVE('',#3127,#3130,#512,.T.);
#4049=EDGE_CURVE('',#3133,#3134,#1967,.T.);
#4050=EDGE_CURVE('',#3134,#3131,#513,.T.);
#4051=EDGE_CURVE('',#3130,#3133,#514,.T.);
#4052=EDGE_CURVE('',#3135,#3136,#1968,.T.);
#4053=EDGE_CURVE('',#3136,#3134,#515,.T.);
#4054=EDGE_CURVE('',#3133,#3135,#516,.T.);
#4055=EDGE_CURVE('',#3137,#3138,#1969,.T.);
#4056=EDGE_CURVE('',#3137,#3139,#517,.T.);
#4057=EDGE_CURVE('',#3140,#3139,#2559,.T.);
#4058=EDGE_CURVE('',#3140,#3138,#518,.T.);
#4059=EDGE_CURVE('',#3141,#3142,#1970,.T.);
#4060=EDGE_CURVE('',#3142,#3143,#519,.T.);
#4061=EDGE_CURVE('',#3144,#3143,#2560,.T.);
#4062=EDGE_CURVE('',#3141,#3144,#520,.T.);
#4063=EDGE_CURVE('',#3145,#3146,#1971,.T.);
#4064=EDGE_CURVE('',#3146,#3142,#521,.T.);
#4065=EDGE_CURVE('',#3145,#3141,#522,.T.);
#4066=EDGE_CURVE('',#3147,#3148,#1972,.T.);
#4067=EDGE_CURVE('',#3148,#3146,#523,.T.);
#4068=EDGE_CURVE('',#3147,#3145,#524,.T.);
#4069=EDGE_CURVE('',#3149,#3150,#1973,.T.);
#4070=EDGE_CURVE('',#3150,#3148,#525,.T.);
#4071=EDGE_CURVE('',#3149,#3147,#526,.T.);
#4072=EDGE_CURVE('',#3151,#3152,#1974,.T.);
#4073=EDGE_CURVE('',#3153,#3151,#527,.T.);
#4074=EDGE_CURVE('',#3154,#3153,#2561,.T.);
#4075=EDGE_CURVE('',#3154,#3152,#528,.T.);
#4076=EDGE_CURVE('',#3152,#3150,#529,.T.);
#4077=EDGE_CURVE('',#3151,#3149,#530,.T.);
#4078=EDGE_CURVE('',#3143,#3129,#531,.T.);
#4079=EDGE_CURVE('',#3139,#3154,#532,.T.);
#4080=EDGE_CURVE('',#3135,#3137,#533,.T.);
#4081=EDGE_CURVE('',#3132,#3144,#534,.T.);
#4082=EDGE_CURVE('',#3138,#3136,#535,.T.);
#4083=EDGE_CURVE('',#3153,#3140,#536,.T.);
#4084=EDGE_CURVE('',#3155,#3156,#1975,.T.);
#4085=EDGE_CURVE('',#3156,#3157,#1976,.T.);
#4086=EDGE_CURVE('',#3157,#3158,#1977,.T.);
#4087=EDGE_CURVE('',#3158,#3159,#1978,.T.);
#4088=EDGE_CURVE('',#3159,#3160,#1979,.T.);
#4089=EDGE_CURVE('',#3160,#3155,#1980,.T.);
#4090=EDGE_CURVE('',#3161,#3162,#1981,.T.);
#4091=EDGE_CURVE('',#3162,#3155,#1982,.T.);
#4092=EDGE_CURVE('',#3161,#3160,#1983,.T.);
#4093=EDGE_CURVE('',#3163,#3161,#1984,.T.);
#4094=EDGE_CURVE('',#3163,#3159,#1985,.T.);
#4095=EDGE_CURVE('',#3164,#3163,#1986,.T.);
#4096=EDGE_CURVE('',#3164,#3158,#1987,.T.);
#4097=EDGE_CURVE('',#3165,#3164,#1988,.T.);
#4098=EDGE_CURVE('',#3165,#3157,#1989,.T.);
#4099=EDGE_CURVE('',#3166,#3165,#1990,.T.);
#4100=EDGE_CURVE('',#3166,#3156,#1991,.T.);
#4101=EDGE_CURVE('',#3162,#3166,#1992,.T.);
#5850=ORIENTED_EDGE('',*,*,#4042,.T.);
#5851=ORIENTED_EDGE('',*,*,#4043,.F.);
#5852=ORIENTED_EDGE('',*,*,#4044,.T.);
#5853=ORIENTED_EDGE('',*,*,#4045,.T.);
#5854=ORIENTED_EDGE('',*,*,#4046,.T.);
#5855=ORIENTED_EDGE('',*,*,#4047,.F.);
#5856=ORIENTED_EDGE('',*,*,#4042,.F.);
#5857=ORIENTED_EDGE('',*,*,#4048,.T.);
#5858=ORIENTED_EDGE('',*,*,#4049,.T.);
#5859=ORIENTED_EDGE('',*,*,#4050,.T.);
#5860=ORIENTED_EDGE('',*,*,#4045,.F.);
#5861=ORIENTED_EDGE('',*,*,#4051,.T.);
#5862=ORIENTED_EDGE('',*,*,#4052,.T.);
#5863=ORIENTED_EDGE('',*,*,#4053,.T.);
#5864=ORIENTED_EDGE('',*,*,#4049,.F.);
#5865=ORIENTED_EDGE('',*,*,#4054,.T.);
#5866=ORIENTED_EDGE('',*,*,#4055,.F.);
#5867=ORIENTED_EDGE('',*,*,#4056,.T.);
#5868=ORIENTED_EDGE('',*,*,#4057,.F.);
#5869=ORIENTED_EDGE('',*,*,#4058,.T.);
#5870=ORIENTED_EDGE('',*,*,#4059,.T.);
#5871=ORIENTED_EDGE('',*,*,#4060,.T.);
#5872=ORIENTED_EDGE('',*,*,#4061,.F.);
#5873=ORIENTED_EDGE('',*,*,#4062,.F.);
#5874=ORIENTED_EDGE('',*,*,#4063,.T.);
#5875=ORIENTED_EDGE('',*,*,#4064,.T.);
#5876=ORIENTED_EDGE('',*,*,#4059,.F.);
#5877=ORIENTED_EDGE('',*,*,#4065,.F.);
#5878=ORIENTED_EDGE('',*,*,#4066,.T.);
#5879=ORIENTED_EDGE('',*,*,#4067,.T.);
#5880=ORIENTED_EDGE('',*,*,#4063,.F.);
#5881=ORIENTED_EDGE('',*,*,#4068,.F.);
#5882=ORIENTED_EDGE('',*,*,#4069,.T.);
#5883=ORIENTED_EDGE('',*,*,#4070,.T.);
#5884=ORIENTED_EDGE('',*,*,#4066,.F.);
#5885=ORIENTED_EDGE('',*,*,#4071,.F.);
#5886=ORIENTED_EDGE('',*,*,#4072,.F.);
#5887=ORIENTED_EDGE('',*,*,#4073,.F.);
#5888=ORIENTED_EDGE('',*,*,#4074,.F.);
#5889=ORIENTED_EDGE('',*,*,#4075,.T.);
#5890=ORIENTED_EDGE('',*,*,#4072,.T.);
#5891=ORIENTED_EDGE('',*,*,#4076,.T.);
#5892=ORIENTED_EDGE('',*,*,#4069,.F.);
#5893=ORIENTED_EDGE('',*,*,#4077,.F.);
#5894=ORIENTED_EDGE('',*,*,#4078,.F.);
#5895=ORIENTED_EDGE('',*,*,#4060,.F.);
#5896=ORIENTED_EDGE('',*,*,#4064,.F.);
#5897=ORIENTED_EDGE('',*,*,#4067,.F.);
#5898=ORIENTED_EDGE('',*,*,#4070,.F.);
#5899=ORIENTED_EDGE('',*,*,#4076,.F.);
#5900=ORIENTED_EDGE('',*,*,#4075,.F.);
#5901=ORIENTED_EDGE('',*,*,#4079,.F.);
#5902=ORIENTED_EDGE('',*,*,#4056,.F.);
#5903=ORIENTED_EDGE('',*,*,#4080,.F.);
#5904=ORIENTED_EDGE('',*,*,#4054,.F.);
#5905=ORIENTED_EDGE('',*,*,#4051,.F.);
#5906=ORIENTED_EDGE('',*,*,#4048,.F.);
#5907=ORIENTED_EDGE('',*,*,#4044,.F.);
#5908=ORIENTED_EDGE('',*,*,#4081,.F.);
#5909=ORIENTED_EDGE('',*,*,#4046,.F.);
#5910=ORIENTED_EDGE('',*,*,#4050,.F.);
#5911=ORIENTED_EDGE('',*,*,#4053,.F.);
#5912=ORIENTED_EDGE('',*,*,#4082,.F.);
#5913=ORIENTED_EDGE('',*,*,#4058,.F.);
#5914=ORIENTED_EDGE('',*,*,#4083,.F.);
#5915=ORIENTED_EDGE('',*,*,#4073,.T.);
#5916=ORIENTED_EDGE('',*,*,#4077,.T.);
#5917=ORIENTED_EDGE('',*,*,#4071,.T.);
#5918=ORIENTED_EDGE('',*,*,#4068,.T.);
#5919=ORIENTED_EDGE('',*,*,#4065,.T.);
#5920=ORIENTED_EDGE('',*,*,#4062,.T.);
#5921=ORIENTED_EDGE('',*,*,#4084,.T.);
#5922=ORIENTED_EDGE('',*,*,#4085,.T.);
#5923=ORIENTED_EDGE('',*,*,#4086,.T.);
#5924=ORIENTED_EDGE('',*,*,#4087,.T.);
#5925=ORIENTED_EDGE('',*,*,#4088,.T.);
#5926=ORIENTED_EDGE('',*,*,#4089,.T.);
#5927=ORIENTED_EDGE('',*,*,#4079,.T.);
#5928=ORIENTED_EDGE('',*,*,#4074,.T.);
#5929=ORIENTED_EDGE('',*,*,#4083,.T.);
#5930=ORIENTED_EDGE('',*,*,#4057,.T.);
#5931=ORIENTED_EDGE('',*,*,#4055,.T.);
#5932=ORIENTED_EDGE('',*,*,#4082,.T.);
#5933=ORIENTED_EDGE('',*,*,#4052,.F.);
#5934=ORIENTED_EDGE('',*,*,#4080,.T.);
#5935=ORIENTED_EDGE('',*,*,#4090,.T.);
#5936=ORIENTED_EDGE('',*,*,#4091,.T.);
#5937=ORIENTED_EDGE('',*,*,#4089,.F.);
#5938=ORIENTED_EDGE('',*,*,#4092,.F.);
#5939=ORIENTED_EDGE('',*,*,#4093,.T.);
#5940=ORIENTED_EDGE('',*,*,#4092,.T.);
#5941=ORIENTED_EDGE('',*,*,#4088,.F.);
#5942=ORIENTED_EDGE('',*,*,#4094,.F.);
#5943=ORIENTED_EDGE('',*,*,#4095,.T.);
#5944=ORIENTED_EDGE('',*,*,#4094,.T.);
#5945=ORIENTED_EDGE('',*,*,#4087,.F.);
#5946=ORIENTED_EDGE('',*,*,#4096,.F.);
#5947=ORIENTED_EDGE('',*,*,#4097,.T.);
#5948=ORIENTED_EDGE('',*,*,#4096,.T.);
#5949=ORIENTED_EDGE('',*,*,#4086,.F.);
#5950=ORIENTED_EDGE('',*,*,#4098,.F.);
#5951=ORIENTED_EDGE('',*,*,#4099,.T.);
#5952=ORIENTED_EDGE('',*,*,#4098,.T.);
#5953=ORIENTED_EDGE('',*,*,#4085,.F.);
#5954=ORIENTED_EDGE('',*,*,#4100,.F.);
#5955=ORIENTED_EDGE('',*,*,#4101,.T.);
#5956=ORIENTED_EDGE('',*,*,#4100,.T.);
#5957=ORIENTED_EDGE('',*,*,#4084,.F.);
#5958=ORIENTED_EDGE('',*,*,#4091,.F.);
#5959=ORIENTED_EDGE('',*,*,#4101,.F.);
#5960=ORIENTED_EDGE('',*,*,#4090,.F.);
#5961=ORIENTED_EDGE('',*,*,#4093,.F.);
#5962=ORIENTED_EDGE('',*,*,#4095,.F.);
#5963=ORIENTED_EDGE('',*,*,#4097,.F.);
#5964=ORIENTED_EDGE('',*,*,#4099,.F.);
#5965=ORIENTED_EDGE('',*,*,#4078,.T.);
#5966=ORIENTED_EDGE('',*,*,#4043,.T.);
#5967=ORIENTED_EDGE('',*,*,#4047,.T.);
#5968=ORIENTED_EDGE('',*,*,#4081,.T.);
#5969=ORIENTED_EDGE('',*,*,#4061,.T.);
#6099=CYLINDRICAL_SURFACE('',#7032,0.12645);
#6100=CYLINDRICAL_SURFACE('',#7034,0.12645);
#6101=CYLINDRICAL_SURFACE('',#7036,0.12645);
#6102=CYLINDRICAL_SURFACE('',#7037,0.12645);
#6103=CYLINDRICAL_SURFACE('',#7038,0.12645);
#6104=CYLINDRICAL_SURFACE('',#7040,0.1543);
#6105=CYLINDRICAL_SURFACE('',#7042,0.1543);
#6106=CYLINDRICAL_SURFACE('',#7043,0.1543);
#6107=CYLINDRICAL_SURFACE('',#7044,0.1543);
#6108=CYLINDRICAL_SURFACE('',#7045,0.1543);
#6109=CYLINDRICAL_SURFACE('',#7047,0.1543);
#6110=CYLINDRICAL_SURFACE('',#7049,0.12645);
#6460=ADVANCED_FACE('',(#1129),#6099,.F.);
#6461=ADVANCED_FACE('',(#1130),#6100,.F.);
#6462=ADVANCED_FACE('',(#1131),#6101,.F.);
#6463=ADVANCED_FACE('',(#1132),#6102,.F.);
#6464=ADVANCED_FACE('',(#1133),#6103,.F.);
#6465=ADVANCED_FACE('',(#1134),#6104,.F.);
#6466=ADVANCED_FACE('',(#1135),#6105,.F.);
#6467=ADVANCED_FACE('',(#1136),#6106,.F.);
#6468=ADVANCED_FACE('',(#1137),#6107,.F.);
#6469=ADVANCED_FACE('',(#1138),#6108,.F.);
#6470=ADVANCED_FACE('',(#1139),#6109,.F.);
#6471=ADVANCED_FACE('',(#1140),#169,.F.);
#6472=ADVANCED_FACE('',(#1141),#170,.F.);
#6473=ADVANCED_FACE('',(#1142,#634),#772,.T.);
#6474=ADVANCED_FACE('',(#1143),#6110,.F.);
#6475=ADVANCED_FACE('',(#1144),#773,.T.);
#6476=ADVANCED_FACE('',(#1145),#774,.T.);
#6477=ADVANCED_FACE('',(#1146),#775,.T.);
#6478=ADVANCED_FACE('',(#1147),#776,.T.);
#6479=ADVANCED_FACE('',(#1148),#777,.T.);
#6480=ADVANCED_FACE('',(#1149),#778,.T.);
#6481=ADVANCED_FACE('',(#1150,#635),#779,.F.);
#6493=CLOSED_SHELL('',(#6460,#6461,#6462,#6463,#6464,#6465,#6466,#6467,
#6468,#6469,#6470,#6471,#6472,#6473,#6474,#6475,#6476,#6477,#6478,#6479,
#6480,#6481));
#7031=AXIS2_PLACEMENT_3D('',#17389,#8328,#8329);
#7032=AXIS2_PLACEMENT_3D('',#17390,#8330,#8331);
#7033=AXIS2_PLACEMENT_3D('',#17395,#8333,#8334);
#7034=AXIS2_PLACEMENT_3D('',#17403,#8335,#8336);
#7035=AXIS2_PLACEMENT_3D('',#17427,#8338,#8339);
#7036=AXIS2_PLACEMENT_3D('',#17450,#8340,#8341);
#7037=AXIS2_PLACEMENT_3D('',#17504,#8343,#8344);
#7038=AXIS2_PLACEMENT_3D('',#17552,#8346,#8347);
#7039=AXIS2_PLACEMENT_3D('',#17571,#8349,#8350);
#7040=AXIS2_PLACEMENT_3D('',#17591,#8351,#8352);
#7041=AXIS2_PLACEMENT_3D('',#17604,#8354,#8355);
#7042=AXIS2_PLACEMENT_3D('',#17612,#8356,#8357);
#7043=AXIS2_PLACEMENT_3D('',#17637,#8359,#8360);
#7044=AXIS2_PLACEMENT_3D('',#17662,#8362,#8363);
#7045=AXIS2_PLACEMENT_3D('',#17687,#8365,#8366);
#7046=AXIS2_PLACEMENT_3D('',#17698,#8368,#8369);
#7047=AXIS2_PLACEMENT_3D('',#17704,#8370,#8371);
#7048=AXIS2_PLACEMENT_3D('',#18260,#8372,#8373);
#7049=AXIS2_PLACEMENT_3D('',#18273,#8380,#8381);
#7050=AXIS2_PLACEMENT_3D('',#18274,#8382,#8383);
#7051=AXIS2_PLACEMENT_3D('',#18280,#8387,#8388);
#7052=AXIS2_PLACEMENT_3D('',#18284,#8391,#8392);
#7053=AXIS2_PLACEMENT_3D('',#18288,#8395,#8396);
#7054=AXIS2_PLACEMENT_3D('',#18292,#8399,#8400);
#7055=AXIS2_PLACEMENT_3D('',#18296,#8403,#8404);
#7056=AXIS2_PLACEMENT_3D('',#18298,#8406,#8407);
#8328=DIRECTION('axis',(0.,0.,1.));
#8329=DIRECTION('refdir',(1.,0.,0.));
#8330=DIRECTION('center_axis',(0.,0.,-1.));
#8331=DIRECTION('ref_axis',(1.,0.,0.));
#8332=DIRECTION('',(0.,0.,-1.));
#8333=DIRECTION('center_axis',(0.,0.,-1.));
#8334=DIRECTION('ref_axis',(1.,0.,0.));
#8335=DIRECTION('center_axis',(0.,0.,-1.));
#8336=DIRECTION('ref_axis',(1.,0.,0.));
#8337=DIRECTION('',(0.,0.,-1.));
#8338=DIRECTION('center_axis',(0.,0.,-1.));
#8339=DIRECTION('ref_axis',(1.,0.,0.));
#8340=DIRECTION('center_axis',(0.,0.,-1.));
#8341=DIRECTION('ref_axis',(1.,0.,0.));
#8342=DIRECTION('',(0.,0.,-1.));
#8343=DIRECTION('center_axis',(0.,0.,-1.));
#8344=DIRECTION('ref_axis',(1.,0.,0.));
#8345=DIRECTION('',(0.,0.,-1.));
#8346=DIRECTION('center_axis',(0.,0.,-1.));
#8347=DIRECTION('ref_axis',(0.937385399639056,-0.348293859468591,0.));
#8348=DIRECTION('',(0.,0.,-1.));
#8349=DIRECTION('center_axis',(0.,0.,-1.));
#8350=DIRECTION('ref_axis',(1.,0.,0.));
#8351=DIRECTION('center_axis',(0.,0.,-1.));
#8352=DIRECTION('ref_axis',(0.28361887368566,0.958937085782627,0.));
#8353=DIRECTION('',(1.22464679914735E-16,8.07419868282478E-31,-1.));
#8354=DIRECTION('center_axis',(0.,0.,1.));
#8355=DIRECTION('ref_axis',(1.,6.71554824363804E-15,0.));
#8356=DIRECTION('center_axis',(0.,0.,-1.));
#8357=DIRECTION('ref_axis',(1.,6.71554824363804E-15,0.));
#8358=DIRECTION('',(1.22464679914735E-16,8.07419868282478E-31,-1.));
#8359=DIRECTION('center_axis',(0.,0.,-1.));
#8360=DIRECTION('ref_axis',(1.,6.71554824363804E-15,0.));
#8361=DIRECTION('',(1.22464679914735E-16,8.07419868282478E-31,-1.));
#8362=DIRECTION('center_axis',(0.,0.,-1.));
#8363=DIRECTION('ref_axis',(1.,6.71554824363804E-15,0.));
#8364=DIRECTION('',(1.22464679914735E-16,8.07419868282478E-31,-1.));
#8365=DIRECTION('center_axis',(0.,0.,-1.));
#8366=DIRECTION('ref_axis',(-0.60895050335979,-0.793208222636313,0.));
#8367=DIRECTION('',(1.22464679914735E-16,8.07419868282478E-31,-1.));
#8368=DIRECTION('center_axis',(0.,0.,-1.));
#8369=DIRECTION('ref_axis',(1.,6.71554824363804E-15,0.));
#8370=DIRECTION('center_axis',(0.,0.,-1.));
#8371=DIRECTION('ref_axis',(1.,6.71554824363804E-15,0.));
#8372=DIRECTION('center_axis',(0.,0.,1.));
#8373=DIRECTION('ref_axis',(1.,0.,0.));
#8374=DIRECTION('',(0.5,0.866025403784439,0.));
#8375=DIRECTION('',(-0.5,0.866025403784439,0.));
#8376=DIRECTION('',(-1.,0.,0.));
#8377=DIRECTION('',(-0.5,-0.866025403784439,0.));
#8378=DIRECTION('',(0.5,-0.866025403784439,0.));
#8379=DIRECTION('',(1.,-3.49629579342466E-16,0.));
#8380=DIRECTION('center_axis',(0.,0.,-1.));
#8381=DIRECTION('ref_axis',(1.,0.,0.));
#8382=DIRECTION('center_axis',(-3.49629579342466E-16,-1.,0.));
#8383=DIRECTION('ref_axis',(1.,-3.49629579342466E-16,0.));
#8384=DIRECTION('',(1.,-3.49629579342466E-16,0.));
#8385=DIRECTION('',(0.,0.,1.));
#8386=DIRECTION('',(0.,0.,1.));
#8387=DIRECTION('center_axis',(-0.866025403784439,-0.5,0.));
#8388=DIRECTION('ref_axis',(0.5,-0.866025403784439,0.));
#8389=DIRECTION('',(0.5,-0.866025403784439,0.));
#8390=DIRECTION('',(0.,0.,1.));
#8391=DIRECTION('center_axis',(-0.866025403784439,0.5,0.));
#8392=DIRECTION('ref_axis',(-0.5,-0.866025403784439,0.));
#8393=DIRECTION('',(-0.5,-0.866025403784439,0.));
#8394=DIRECTION('',(0.,0.,1.));
#8395=DIRECTION('center_axis',(0.,1.,0.));
#8396=DIRECTION('ref_axis',(-1.,0.,0.));
#8397=DIRECTION('',(-1.,0.,0.));
#8398=DIRECTION('',(0.,0.,1.));
#8399=DIRECTION('center_axis',(0.866025403784439,0.5,0.));
#8400=DIRECTION('ref_axis',(-0.5,0.866025403784439,0.));
#8401=DIRECTION('',(-0.5,0.866025403784439,0.));
#8402=DIRECTION('',(0.,0.,1.));
#8403=DIRECTION('center_axis',(0.866025403784439,-0.5,0.));
#8404=DIRECTION('ref_axis',(0.5,0.866025403784439,0.));
#8405=DIRECTION('',(0.5,0.866025403784439,0.));
#8406=DIRECTION('center_axis',(0.,0.,1.));
#8407=DIRECTION('ref_axis',(1.,0.,0.));
#17389=CARTESIAN_POINT('',(0.,0.,0.));
#17390=CARTESIAN_POINT('Origin',(0.,0.,0.12));
#17391=CARTESIAN_POINT('',(-0.12639138516214,8.91322620741042E-5,0.00934196736194174));
#17392=CARTESIAN_POINT('',(-0.12645,1.54856587752183E-17,-5.55111512312578E-17));
#17393=CARTESIAN_POINT('',(-0.12645,1.54856587752183E-17,0.12));
#17394=CARTESIAN_POINT('',(-0.0488748409397564,0.116622692573588,0.));
#17395=CARTESIAN_POINT('Origin',(0.,0.,0.));
#17396=CARTESIAN_POINT('Ctrl Pts',(-0.0489111879062984,0.116810626195002,
1.20007714660797E-17));
#17397=CARTESIAN_POINT('Ctrl Pts',(-0.0838963038512042,0.101957324585112,
0.00240024091002088));
#17398=CARTESIAN_POINT('Ctrl Pts',(-0.11198221847721,0.0702793053867637,
0.00480048182004174));
#17399=CARTESIAN_POINT('Ctrl Pts',(-0.122072221370749,0.0336561163696377,
0.00720072273006261));
#17400=CARTESIAN_POINT('Ctrl Pts',(-0.125072637487486,0.022765653033531,
0.00791447094068899));
#17401=CARTESIAN_POINT('Ctrl Pts',(-0.126481745582665,0.0114379076904012,
0.00862821915131536));
#17402=CARTESIAN_POINT('Ctrl Pts',(-0.12639138516214,8.91322620741042E-5,
0.00934196736194174));
#17403=CARTESIAN_POINT('Origin',(0.,0.,0.12));
#17404=CARTESIAN_POINT('',(-0.126396145829628,-9.95859796292312E-5,0.0593419673619417));
#17405=CARTESIAN_POINT('',(-0.126575671592806,-7.20628672610732E-5,0.0456580326380584));
#17406=CARTESIAN_POINT('',(-0.12645,1.54856587752183E-17,0.12));
#17407=CARTESIAN_POINT('',(-0.10808967569503,-0.0656218295092665,0.));
#17408=CARTESIAN_POINT('Ctrl Pts',(-0.126575671592806,-7.20628672610732E-5,
0.0456580326380584));
#17409=CARTESIAN_POINT('Ctrl Pts',(-0.126327459688109,0.0361497101693465,
0.0433719816070355));
#17410=CARTESIAN_POINT('Ctrl Pts',(-0.109912066394173,0.0725710138228805,
0.0410859305760125));
#17411=CARTESIAN_POINT('Ctrl Pts',(-0.0824515099939393,0.0961223418729112,
0.0387998795449896));
#17412=CARTESIAN_POINT('Ctrl Pts',(-0.05137998778939,0.122770586059505,
0.036213220908657));
#17413=CARTESIAN_POINT('Ctrl Pts',(-0.00616751748104999,0.132941603485868,
0.0336265622723243));
#17414=CARTESIAN_POINT('Ctrl Pts',(0.0333172074018229,0.122176268745047,
0.0310399036359917));
#17415=CARTESIAN_POINT('Ctrl Pts',(0.0728019322846963,0.111410934004226,
0.028453244999659));
#17416=CARTESIAN_POINT('Ctrl Pts',(0.106558911742102,0.0797092470962188,
0.0258665863633264));
#17417=CARTESIAN_POINT('Ctrl Pts',(0.11981357554495,0.0409763259700822,
0.0232799277269937));
#17418=CARTESIAN_POINT('Ctrl Pts',(0.133068239347797,0.00224340484394604,
0.0206932690906611));
#17419=CARTESIAN_POINT('Ctrl Pts',(0.125820587496086,-0.0435207505003201,
0.0181066104543285));
#17420=CARTESIAN_POINT('Ctrl Pts',(0.101166903546451,-0.0762076816581678,
0.0155199518179958));
#17421=CARTESIAN_POINT('Ctrl Pts',(0.0765132195968157,-0.108894612816016,
0.0129332931816632));
#17422=CARTESIAN_POINT('Ctrl Pts',(0.0344535035492562,-0.128504319787445,
0.0103466345453306));
#17423=CARTESIAN_POINT('Ctrl Pts',(-0.00636464094143544,-0.126469737202777,
0.00775997590899791));
#17424=CARTESIAN_POINT('Ctrl Pts',(-0.0471827854321269,-0.124435154618108,
0.00517331727266527));
#17425=CARTESIAN_POINT('Ctrl Pts',(-0.0867593583659505,-0.100756282477341,
0.00258665863633259));
#17426=CARTESIAN_POINT('Ctrl Pts',(-0.108089675695031,-0.0656218295092657,
-5.55111512312578E-17));
#17427=CARTESIAN_POINT('Origin',(0.,0.,0.));
#17428=CARTESIAN_POINT('Ctrl Pts',(-0.12639138516214,8.91322620741042E-5,
0.00934196736194174));
#17429=CARTESIAN_POINT('Ctrl Pts',(-0.126154274972366,-0.0296906128949183,
0.011214877787648));
#17430=CARTESIAN_POINT('Ctrl Pts',(-0.115592373032178,-0.0596151635265703,
0.0130877882133543));
#17431=CARTESIAN_POINT('Ctrl Pts',(-0.0963650578556872,-0.0821635787359664,
0.0149606986390606));
#17432=CARTESIAN_POINT('Ctrl Pts',(-0.0698103971670931,-0.113304978845907,
0.0175473572753932));
#17433=CARTESIAN_POINT('Ctrl Pts',(-0.0267272342632827,-0.130377059081323,
0.0201340159117258));
#17434=CARTESIAN_POINT('Ctrl Pts',(0.0139574509341311,-0.125868770046104,
0.0227206745480584));
#17435=CARTESIAN_POINT('Ctrl Pts',(0.0546421361315456,-0.121360481010885,
0.0253073331843911));
#17436=CARTESIAN_POINT('Ctrl Pts',(0.0929283436225635,-0.0952718227050311,
0.0278939918207237));
#17437=CARTESIAN_POINT('Ctrl Pts',(0.112018291148455,-0.0590635258734944,
0.0304806504570564));
#17438=CARTESIAN_POINT('Ctrl Pts',(0.131108238674346,-0.0228552290419586,
0.033067309093389));
#17439=CARTESIAN_POINT('Ctrl Pts',(0.131001926235112,0.0234727063152593,
0.0356539677297216));
#17440=CARTESIAN_POINT('Ctrl Pts',(0.111741771403992,0.0595891814911641,
0.0382406263660542));
#17441=CARTESIAN_POINT('Ctrl Pts',(0.0924816165728724,0.0957056566670696,
0.0408272850023869));
#17442=CARTESIAN_POINT('Ctrl Pts',(0.0540676193498672,0.121610671661662,
0.0434139436387195));
#17443=CARTESIAN_POINT('Ctrl Pts',(0.0133639835211523,0.125930636937597,
0.0460006022750522));
#17444=CARTESIAN_POINT('Ctrl Pts',(-0.0273396523075625,0.130250602213533,
0.0485872609113848));
#17445=CARTESIAN_POINT('Ctrl Pts',(-0.0703329267419868,0.112985517770812,
0.0511739195477175));
#17446=CARTESIAN_POINT('Ctrl Pts',(-0.0967449447385466,0.0817152626609385,
0.0537605781840501));
#17447=CARTESIAN_POINT('Ctrl Pts',(-0.115741878896724,0.0592240248649833,
0.0556210412433473));
#17448=CARTESIAN_POINT('Ctrl Pts',(-0.126160906676814,0.0294875554882879,
0.0574815043026445));
#17449=CARTESIAN_POINT('Ctrl Pts',(-0.126396145829628,-9.95859796292312E-5,
0.0593419673619417));
#17450=CARTESIAN_POINT('Origin',(0.,0.,0.12));
#17451=CARTESIAN_POINT('',(-0.126529791093031,9.025049583615E-5,0.109341967361942));
#17452=CARTESIAN_POINT('',(-0.126349242904067,8.85860673823967E-5,0.0956580326380584));
#17453=CARTESIAN_POINT('',(-0.12645,1.54856587752183E-17,0.12));
#17454=CARTESIAN_POINT('Ctrl Pts',(-0.126349242904067,8.85860673823967E-5,
0.0956580326380584));
#17455=CARTESIAN_POINT('Ctrl Pts',(-0.126441591528965,0.0135570965972842,
0.0948119253946973));
#17456=CARTESIAN_POINT('Ctrl Pts',(-0.124448136217638,0.0269990101701626,
0.0939658181513361));
#17457=CARTESIAN_POINT('Ctrl Pts',(-0.120249444863787,0.0397126388809939,
0.093119710907975));
#17458=CARTESIAN_POINT('Ctrl Pts',(-0.107413505522824,0.0785798365820317,
0.0905330522716423));
#17459=CARTESIAN_POINT('Ctrl Pts',(-0.0739673525896496,0.110640458354997,
0.0879463936353097));
#17460=CARTESIAN_POINT('Ctrl Pts',(-0.0345920580258737,0.121821308595361,
0.085359734998977));
#17461=CARTESIAN_POINT('Ctrl Pts',(0.00478323653790218,0.133002158835724,
0.0827730763626444));
#17462=CARTESIAN_POINT('Ctrl Pts',(0.0500876727322792,0.123303237543486,
0.0801864177263117));
#17463=CARTESIAN_POINT('Ctrl Pts',(0.0814342209129887,0.0969820390626645,
0.077599759089979));
#17464=CARTESIAN_POINT('Ctrl Pts',(0.112780769093698,0.0706608405818426,
0.0750131004536464));
#17465=CARTESIAN_POINT('Ctrl Pts',(0.13016942926074,0.0277173649124373,
0.0724264418173139));
#17466=CARTESIAN_POINT('Ctrl Pts',(0.12596827751407,-0.0129984006283456,
0.0698397831809812));
#17467=CARTESIAN_POINT('Ctrl Pts',(0.121767125767399,-0.0537141661691284,
0.0672531245446486));
#17468=CARTESIAN_POINT('Ctrl Pts',(0.0959761621070158,-0.0922022215812886,
0.0646664659083159));
#17469=CARTESIAN_POINT('Ctrl Pts',(0.059914723710966,-0.111567668284471,
0.0620798072719833));
#17470=CARTESIAN_POINT('Ctrl Pts',(0.0238532853149157,-0.130933114987654,
0.0594931486356506));
#17471=CARTESIAN_POINT('Ctrl Pts',(-0.0224786278168013,-0.131175952981858,
0.056906489999318));
#17472=CARTESIAN_POINT('Ctrl Pts',(-0.0587401909579078,-0.112190380850839,
0.0543198313629853));
#17473=CARTESIAN_POINT('Ctrl Pts',(-0.0950017540990138,-0.0932048087198191,
0.0517331727266527));
#17474=CARTESIAN_POINT('Ctrl Pts',(-0.12119296724951,-0.0549908264635757,
0.0491465140903201));
#17475=CARTESIAN_POINT('Ctrl Pts',(-0.125823286774378,-0.0143210998620416,
0.0465598554539874));
#17476=CARTESIAN_POINT('Ctrl Pts',(-0.126361397696569,-0.0095946821776348,
0.0462592478486778));
#17477=CARTESIAN_POINT('Ctrl Pts',(-0.12660831057823,-0.00483509759607578,
0.0459586402433681));
#17478=CARTESIAN_POINT('Ctrl Pts',(-0.126575671592806,-7.20628672610732E-5,
0.0456580326380584));
#17479=CARTESIAN_POINT('Ctrl Pts',(-0.126396145829628,-9.95859796292312E-5,
0.0593419673619417));
#17480=CARTESIAN_POINT('Ctrl Pts',(-0.12648796685852,-0.0116483513064931,
0.0600681629389771));
#17481=CARTESIAN_POINT('Ctrl Pts',(-0.125028206814926,-0.0231743653405588,
0.0607943585160125));
#17482=CARTESIAN_POINT('Ctrl Pts',(-0.121921363946098,-0.034237873926493,
0.0615205540930479));
#17483=CARTESIAN_POINT('Ctrl Pts',(-0.110855003598394,-0.0736453296270277,
0.0641072127293806));
#17484=CARTESIAN_POINT('Ctrl Pts',(-0.0788915213442898,-0.107184815251071,
0.0666938713657133));
#17485=CARTESIAN_POINT('Ctrl Pts',(-0.0400617348236378,-0.120133683626334,
0.069280530002046));
#17486=CARTESIAN_POINT('Ctrl Pts',(-0.00123194830298627,-0.133082552001597,
0.0718671886383786));
#17487=CARTESIAN_POINT('Ctrl Pts',(0.0444641424842127,-0.125440803128081,
0.0744538472747112));
#17488=CARTESIAN_POINT('Ctrl Pts',(0.0769682295152699,-0.100563001286921,
0.0770405059110438));
#17489=CARTESIAN_POINT('Ctrl Pts',(0.109472316546327,-0.0756851994457607,
0.0796271645473764));
#17490=CARTESIAN_POINT('Ctrl Pts',(0.128784399821243,-0.0335713446369571,
0.0822138231837091));
#17491=CARTESIAN_POINT('Ctrl Pts',(0.126427276285523,0.00729262199647547,
0.0848004818200417));
#17492=CARTESIAN_POINT('Ctrl Pts',(0.124070152749803,0.0481565886299079,
0.0873871404563744));
#17493=CARTESIAN_POINT('Ctrl Pts',(0.100043822403448,0.0877706670879697,
0.0899737990927071));
#17494=CARTESIAN_POINT('Ctrl Pts',(0.0648947831756147,0.108746049780439,
0.0925604577290397));
#17495=CARTESIAN_POINT('Ctrl Pts',(0.0297457439477817,0.129721432472907,
0.0951471163653723));
#17496=CARTESIAN_POINT('Ctrl Pts',(-0.0165260041615291,0.132058119399784,
0.0977337750017049));
#17497=CARTESIAN_POINT('Ctrl Pts',(-0.0536093211433369,0.114730442741844,
0.100320433638038));
#17498=CARTESIAN_POINT('Ctrl Pts',(-0.0906926381251451,0.0974027660839045,
0.10290709227437));
#17499=CARTESIAN_POINT('Ctrl Pts',(-0.11858752397945,0.0604107258411485,
0.105493750910703));
#17500=CARTESIAN_POINT('Ctrl Pts',(-0.12504939731921,0.0199921027543164,
0.108080409547035));
#17501=CARTESIAN_POINT('Ctrl Pts',(-0.126099919499473,0.0134211506765118,
0.108500928818671));
#17502=CARTESIAN_POINT('Ctrl Pts',(-0.126583971845017,0.00675963476331471,
0.108921448090306));
#17503=CARTESIAN_POINT('Ctrl Pts',(-0.126529791093031,9.025049583615E-5,
0.109341967361942));
#17504=CARTESIAN_POINT('Origin',(0.,0.,0.12));
#17505=CARTESIAN_POINT('',(-0.126296536029262,-6.10717992316628E-5,0.159341967361942));
#17506=CARTESIAN_POINT('',(-0.126453631260982,-0.000102348163238207,0.145658032638058));
#17507=CARTESIAN_POINT('',(-0.12645,1.54856587752183E-17,0.12));
#17508=CARTESIAN_POINT('Ctrl Pts',(-0.126453631260982,-0.000102348163238207,
0.145658032638058));
#17509=CARTESIAN_POINT('Ctrl Pts',(-0.126183364177612,0.031552920325249,
0.143665210546026));
#17510=CARTESIAN_POINT('Ctrl Pts',(-0.114073771100105,0.0633928690595716,
0.141672388453994));
#17511=CARTESIAN_POINT('Ctrl Pts',(-0.0925489356314354,0.0864391430514358,
0.139679566361962));
#17512=CARTESIAN_POINT('Ctrl Pts',(-0.0646099631645552,0.116352924063146,
0.13709290772563));
#17513=CARTESIAN_POINT('Ctrl Pts',(-0.0208084524006029,0.131451366650306,
0.134506249089297));
#17514=CARTESIAN_POINT('Ctrl Pts',(0.0196287675426836,0.125106932552633,
0.131919590452964));
#17515=CARTESIAN_POINT('Ctrl Pts',(0.0600659874859703,0.11876249845496,
0.129332931816632));
#17516=CARTESIAN_POINT('Ctrl Pts',(0.097138916608591,0.0909751876724545,
0.126746273180299));
#17517=CARTESIAN_POINT('Ctrl Pts',(0.114574233156503,0.0539423598350403,
0.124159614543967));
#17518=CARTESIAN_POINT('Ctrl Pts',(0.132009549704415,0.0169095319976262,
0.121572955907634));
#17519=CARTESIAN_POINT('Ctrl Pts',(0.129807253677619,-0.0293688128946969,
0.118986297271301));
#17520=CARTESIAN_POINT('Ctrl Pts',(0.108934072954415,-0.0645786240759305,
0.116399638634969));
#17521=CARTESIAN_POINT('Ctrl Pts',(0.0880608922312115,-0.099788435257164,
0.113812979998636));
#17522=CARTESIAN_POINT('Ctrl Pts',(0.0485168268116012,-0.123929712727308,
0.111226321362303));
#17523=CARTESIAN_POINT('Ctrl Pts',(0.00765986125275547,-0.126405537442516,
0.108639662725971));
#17524=CARTESIAN_POINT('Ctrl Pts',(-0.0331971043060904,-0.128881362157723,
0.106053004089638));
#17525=CARTESIAN_POINT('Ctrl Pts',(-0.0753669700041717,-0.109691734117994,
0.103466345453305));
#17526=CARTESIAN_POINT('Ctrl Pts',(-0.100339039978837,-0.0772600332835736,
0.100879686816973));
#17527=CARTESIAN_POINT('Ctrl Pts',(-0.117142637704978,-0.0554368822612891,
0.0991391354240014));
#17528=CARTESIAN_POINT('Ctrl Pts',(-0.126159269908366,-0.0276178718881664,
0.0973985840310299));
#17529=CARTESIAN_POINT('Ctrl Pts',(-0.126349242904067,8.85860673823967E-5,
0.0956580326380584));
#17530=CARTESIAN_POINT('Ctrl Pts',(-0.126529791093031,9.025049583615E-5,
0.109341967361942));
#17531=CARTESIAN_POINT('Ctrl Pts',(-0.126250700293628,-0.0342644551610371,
0.111508106726639));
#17532=CARTESIAN_POINT('Ctrl Pts',(-0.111690189779818,-0.0688279388928191,
0.113674246091336));
#17533=CARTESIAN_POINT('Ctrl Pts',(-0.0867076257192948,-0.092297473337895,
0.115840385456033));
#17534=CARTESIAN_POINT('Ctrl Pts',(-0.0568751199544048,-0.120323220412367,
0.118427044092366));
#17535=CARTESIAN_POINT('Ctrl Pts',(-0.0121812475994092,-0.132529508630403,
0.121013702728699));
#17536=CARTESIAN_POINT('Ctrl Pts',(0.0277554439013372,-0.123558363290506,
0.123600361365031));
#17537=CARTESIAN_POINT('Ctrl Pts',(0.0676921354020838,-0.114587217950609,
0.126187020001364));
#17538=CARTESIAN_POINT('Ctrl Pts',(0.102871646048582,-0.0844386390527785,
0.128773678637697));
#17539=CARTESIAN_POINT('Ctrl Pts',(0.117851793294146,-0.0463464242807743,
0.131360337274029));
#17540=CARTESIAN_POINT('Ctrl Pts',(0.13283194053971,-0.00825420950877041,
0.133946995910362));
#17541=CARTESIAN_POINT('Ctrl Pts',(0.127612724384341,0.0377816411374068,
0.136533654546694));
#17542=CARTESIAN_POINT('Ctrl Pts',(0.104485135941302,0.0715534408109559,
0.139120313183027));
#17543=CARTESIAN_POINT('Ctrl Pts',(0.0813575474982633,0.105325240484505,
0.14170697181936));
#17544=CARTESIAN_POINT('Ctrl Pts',(0.0403215867675544,0.126832989185426,
0.144293630455692));
#17545=CARTESIAN_POINT('Ctrl Pts',(-0.000609841963000384,0.126635909896556,
0.146880289092025));
#17546=CARTESIAN_POINT('Ctrl Pts',(-0.0415412706935549,0.126438830607686,
0.149466947728358));
#17547=CARTESIAN_POINT('Ctrl Pts',(-0.0823681674239554,0.104536923329025,
0.15205360636469));
#17548=CARTESIAN_POINT('Ctrl Pts',(-0.10516942503222,0.0705438627883669,
0.154640265001023));
#17549=CARTESIAN_POINT('Ctrl Pts',(-0.118984510025511,0.0499477610899654,
0.156207499121329));
#17550=CARTESIAN_POINT('Ctrl Pts',(-0.126182304652747,0.0249129445447297,
0.157774733241635));
#17551=CARTESIAN_POINT('Ctrl Pts',(-0.126296536029262,-6.10717992316628E-5,
0.159341967361942));
#17552=CARTESIAN_POINT('Origin',(0.,0.,0.12));
#17553=CARTESIAN_POINT('',(-0.126625441102054,2.7778768752873E-5,0.209341967361942));
#17554=CARTESIAN_POINT('',(-0.126471935391749,0.000101176582396995,0.195658032638058));
#17555=CARTESIAN_POINT('',(-0.12645,1.54856587752183E-17,0.12));
#17556=CARTESIAN_POINT('',(0.0958116152722397,0.0825211298936481,0.24));
#17557=CARTESIAN_POINT('Ctrl Pts',(-0.126625441102054,2.7778768752873E-5,
0.209341967361942));
#17558=CARTESIAN_POINT('Ctrl Pts',(-0.126482885932031,-0.0388928622545336,
0.21180133566563));
#17559=CARTESIAN_POINT('Ctrl Pts',(-0.107125339127294,-0.077921419747323,
0.214260703969318));
#17560=CARTESIAN_POINT('Ctrl Pts',(-0.0759952538809665,-0.101287130411732,
0.216720072273006));
#17561=CARTESIAN_POINT('Ctrl Pts',(-0.0432539585932993,-0.12586218783339,
0.219306730909339));
#17562=CARTESIAN_POINT('Ctrl Pts',(0.0025100419330305,-0.133111106253138,
0.221893389545672));
#17563=CARTESIAN_POINT('Ctrl Pts',(0.0412155518054008,-0.119764891216682,
0.224480048182004));
#17564=CARTESIAN_POINT('Ctrl Pts',(0.0799210616777711,-0.106418676180227,
0.227066706818337));
#17565=CARTESIAN_POINT('Ctrl Pts',(0.111568080896182,-0.072477327687567,
0.229653365454669));
#17566=CARTESIAN_POINT('Ctrl Pts',(0.122246574267713,-0.0330282462555153,
0.232240024091002));
#17567=CARTESIAN_POINT('Ctrl Pts',(0.132925067639245,0.00642083517653631,
0.234826682727335));
#17568=CARTESIAN_POINT('Ctrl Pts',(0.122635035163896,0.0513776495479799,
0.237413341363667));
#17569=CARTESIAN_POINT('Ctrl Pts',(0.0958116152722397,0.0825211298936481,
0.24));
#17570=CARTESIAN_POINT('',(-0.0959791030802601,0.0826138105732953,0.24));
#17571=CARTESIAN_POINT('Origin',(0.,0.,0.24));
#17572=CARTESIAN_POINT('Ctrl Pts',(-0.0959791030802601,0.0826138105732953,
0.24));
#17573=CARTESIAN_POINT('Ctrl Pts',(-0.0710417758635208,0.111296717646776,
0.237599759089979));
#17574=CARTESIAN_POINT('Ctrl Pts',(-0.0322351762885183,0.128218895525122,
0.235199518179958));
#17575=CARTESIAN_POINT('Ctrl Pts',(0.00571352152256588,0.126497857083363,
0.232799277269937));
#17576=CARTESIAN_POINT('Ctrl Pts',(0.0466095526337785,0.124643152028446,
0.230212618633605));
#17577=CARTESIAN_POINT('Ctrl Pts',(0.0865092470399708,0.101136876245298,
0.227625959997272));
#17578=CARTESIAN_POINT('Ctrl Pts',(0.107920636628548,0.0662586835305903,
0.225039301360939));
#17579=CARTESIAN_POINT('Ctrl Pts',(0.129332026217125,0.0313804908158828,
0.222452642724607));
#17580=CARTESIAN_POINT('Ctrl Pts',(0.132255110988087,-0.014869618830384,
0.219865984088274));
#17581=CARTESIAN_POINT('Ctrl Pts',(0.115395215428634,-0.0521699181865619,
0.217279325451942));
#17582=CARTESIAN_POINT('Ctrl Pts',(0.0985353198691812,-0.0894702175427398,
0.214692666815609));
#17583=CARTESIAN_POINT('Ctrl Pts',(0.0618924439793129,-0.117820706608829,
0.212106008179276));
#17584=CARTESIAN_POINT('Ctrl Pts',(0.0215571925812854,-0.12478734248304,
0.209519349542944));
#17585=CARTESIAN_POINT('Ctrl Pts',(-0.0187780588167422,-0.13175397835725,
0.206932690906611));
#17586=CARTESIAN_POINT('Ctrl Pts',(-0.0628056857229291,-0.117336761039583,
0.204346032270278));
#17587=CARTESIAN_POINT('Ctrl Pts',(-0.0912027768750998,-0.0878586653637446,
0.201759373633946));
#17588=CARTESIAN_POINT('Ctrl Pts',(-0.113530209130371,-0.0646812849521466,
0.199725593301983));
#17589=CARTESIAN_POINT('Ctrl Pts',(-0.126194825294183,-0.0321932513395888,
0.197691812970021));
#17590=CARTESIAN_POINT('Ctrl Pts',(-0.126471935391749,0.000101176582396995,
0.195658032638058));
#17591=CARTESIAN_POINT('Origin',(0.,0.,0.350421172358873));
#17592=CARTESIAN_POINT('',(-0.154453350152392,-8.79343647196378E-5,0.0295788276411275));
#17593=CARTESIAN_POINT('',(-0.15422847552802,0.000108763211052777,0.025421172358873));
#17594=CARTESIAN_POINT('',(-0.1543,-1.01731279388251E-15,0.350421172358873));
#17595=CARTESIAN_POINT('',(0.15408394018464,-0.00816268198427004,0.));
#17596=CARTESIAN_POINT('Ctrl Pts',(-0.15422847552802,0.000108763211052763,
0.025421172358873));
#17597=CARTESIAN_POINT('Ctrl Pts',(-0.154338737393477,0.0139570514561378,
0.0247074241482466));
#17598=CARTESIAN_POINT('Ctrl Pts',(-0.146387882101843,0.0778735560251454,
0.0214070173012875));
#17599=CARTESIAN_POINT('Ctrl Pts',(-0.0581466660421577,0.171532975008042,
0.0155199518179959));
#17600=CARTESIAN_POINT('Ctrl Pts',(0.109502662757235,0.144085240745689,
0.00775997590899784));
#17601=CARTESIAN_POINT('Ctrl Pts',(0.156737212705124,0.0419221657566679,
0.00258665863633264));
#17602=CARTESIAN_POINT('Ctrl Pts',(0.15408394018464,-0.00816268198427004,
0.));
#17603=CARTESIAN_POINT('',(0.129620323775263,-0.0841289546921688,3.62607491890453E-17));
#17604=CARTESIAN_POINT('Origin',(0.,0.,0.));
#17605=CARTESIAN_POINT('Ctrl Pts',(-0.154453350152392,-8.7934364719636E-5,
0.0295788276411275));
#17606=CARTESIAN_POINT('Ctrl Pts',(-0.154150470777978,0.0441115087317509,
0.0272927766101045));
#17607=CARTESIAN_POINT('Ctrl Pts',(-0.111454882743928,0.138841433785012,
0.0224200669427489));
#17608=CARTESIAN_POINT('Ctrl Pts',(0.0476444145610997,0.174632482457551,
0.0149606986390605));
#17609=CARTESIAN_POINT('Ctrl Pts',(0.168251138196633,0.0613688951001999,
0.0073871404563744));
#17610=CARTESIAN_POINT('Ctrl Pts',(0.154676764047789,-0.0451013867871701,
0.00240024091002087));
#17611=CARTESIAN_POINT('Ctrl Pts',(0.129620323775263,-0.0841289546921688,
1.57209315010398E-17));
#17612=CARTESIAN_POINT('Origin',(0.,0.,0.350421172358873));
#17613=CARTESIAN_POINT('',(-0.154177051641736,0.000108096719625833,0.0795788276411275));
#17614=CARTESIAN_POINT('',(-0.154234284709463,-0.000121519309271207,0.075421172358873));
#17615=CARTESIAN_POINT('',(-0.1543,-1.01731279388251E-15,0.350421172358873));
#17616=CARTESIAN_POINT('Ctrl Pts',(-0.154234284709463,-0.000121519309271208,
0.0754211723588731));
#17617=CARTESIAN_POINT('Ctrl Pts',(-0.153947235272697,0.0359820467524117,
0.0735607092995758));
#17618=CARTESIAN_POINT('Ctrl Pts',(-0.123557126730793,0.122717061869437,
0.0691135876039459));
#17619=CARTESIAN_POINT('Ctrl Pts',(0.0191012565771036,0.180005302104073,
0.0620798072719832));
#17620=CARTESIAN_POINT('Ctrl Pts',(0.159724738700703,0.0851738948996701,
0.0543198313629854));
#17621=CARTESIAN_POINT('Ctrl Pts',(0.160113920417758,-0.0844204212478698,
0.0465598554539874));
#17622=CARTESIAN_POINT('Ctrl Pts',(0.0199582426985643,-0.179924098035372,
0.0387998795449896));
#17623=CARTESIAN_POINT('Ctrl Pts',(-0.123251388539896,-0.123176028715441,
0.0317536518466181));
#17624=CARTESIAN_POINT('Ctrl Pts',(-0.153939142967466,-0.0362298265692857,
0.0272940827845792));
#17625=CARTESIAN_POINT('Ctrl Pts',(-0.15422847552802,0.000108763211052763,
0.025421172358873));
#17626=CARTESIAN_POINT('Ctrl Pts',(-0.154177051641736,0.000108096719625859,
0.0795788276411275));
#17627=CARTESIAN_POINT('Ctrl Pts',(-0.154289739603949,0.0165429814548096,
0.0787327203977663));
#17628=CARTESIAN_POINT('Ctrl Pts',(-0.144420757340354,0.0830897487115299,
0.0752999545180725));
#17629=CARTESIAN_POINT('Ctrl Pts',(-0.0494457976037486,0.174130301808973,
0.0692805300020459));
#17630=CARTESIAN_POINT('Ctrl Pts',(0.11640175885633,0.13862511662766,0.061520554093048));
#17631=CARTESIAN_POINT('Ctrl Pts',(0.18005704388064,-0.0185795878987759,
0.0537605781840501));
#17632=CARTESIAN_POINT('Ctrl Pts',(0.0856431484406112,-0.159474177462153,
0.0460006022750521));
#17633=CARTESIAN_POINT('Ctrl Pts',(-0.0839657292871194,-0.160363143120653,
0.0382406263660544));
#17634=CARTESIAN_POINT('Ctrl Pts',(-0.151599316432495,-0.0616831513139142,
0.0327667014880793));
#17635=CARTESIAN_POINT('Ctrl Pts',(-0.154493177716258,-0.00590000442131094,
0.0298794352464371));
#17636=CARTESIAN_POINT('Ctrl Pts',(-0.154453350152392,-8.7934364719636E-5,
0.0295788276411275));
#17637=CARTESIAN_POINT('Origin',(0.,0.,0.350421172358873));
#17638=CARTESIAN_POINT('',(-0.154304431028624,-0.000124889850439479,0.129578827641127));
#17639=CARTESIAN_POINT('',(-0.154397364694779,0.000110127730384366,0.125421172358873));
#17640=CARTESIAN_POINT('',(-0.1543,-1.01731279388251E-15,0.350421172358873));
#17641=CARTESIAN_POINT('Ctrl Pts',(-0.154397364694779,0.000110127730384357,
0.125421172358873));
#17642=CARTESIAN_POINT('Ctrl Pts',(-0.154463478494948,0.00824841157753406,
0.125000653087238));
#17643=CARTESIAN_POINT('Ctrl Pts',(-0.150239588102603,0.0663774823757793,
0.121993475179269));
#17644=CARTESIAN_POINT('Ctrl Pts',(-0.0766286530280003,0.163994611436961,
0.116399638634969));
#17645=CARTESIAN_POINT('Ctrl Pts',(0.0927599764682439,0.155440618724813,
0.108639662725971));
#17646=CARTESIAN_POINT('Ctrl Pts',(0.180714016146597,0.0104239566588842,
0.100879686816973));
#17647=CARTESIAN_POINT('Ctrl Pts',(0.11001758793024,-0.143743725357685,
0.093119710907975));
#17648=CARTESIAN_POINT('Ctrl Pts',(-0.0572637123892103,-0.171718146500831,
0.0853597349989769));
#17649=CARTESIAN_POINT('Ctrl Pts',(-0.146220320052713,-0.0783754111826042,
0.0794602221492764));
#17650=CARTESIAN_POINT('Ctrl Pts',(-0.154346328875204,-0.0142138442593302,
0.0761473679359084));
#17651=CARTESIAN_POINT('Ctrl Pts',(-0.154234284709463,-0.000121519309271208,
0.0754211723588731));
#17652=CARTESIAN_POINT('Ctrl Pts',(-0.154304431028624,-0.000124889850439474,
0.129578827641127));
#17653=CARTESIAN_POINT('Ctrl Pts',(-0.153974638929265,0.0385022981904757,
0.127586005549095));
#17654=CARTESIAN_POINT('Ctrl Pts',(-0.120018027207353,0.127784966030512,
0.123006524820731));
#17655=CARTESIAN_POINT('Ctrl Pts',(0.0280571680938306,0.178826694862324,
0.115840385456033));
#17656=CARTESIAN_POINT('Ctrl Pts',(0.163771354656592,0.0771047007047774,
0.108080409547035));
#17657=CARTESIAN_POINT('Ctrl Pts',(0.155709331479018,-0.0923080778690166,
0.100320433638038));
#17658=CARTESIAN_POINT('Ctrl Pts',(0.0109489686262093,-0.180682908560435,
0.0925604577290397));
#17659=CARTESIAN_POINT('Ctrl Pts',(-0.126591758993125,-0.118094248159534,
0.0856465890634029));
#17660=CARTESIAN_POINT('Ctrl Pts',(-0.153945238013925,-0.0337005743957639,
0.0813193790340989));
#17661=CARTESIAN_POINT('Ctrl Pts',(-0.154177051641736,0.000108096719625859,
0.0795788276411275));
#17662=CARTESIAN_POINT('Origin',(0.,0.,0.350421172358873));
#17663=CARTESIAN_POINT('',(-0.154326766555531,0.000123460234585843,0.179578827641127));
#17664=CARTESIAN_POINT('',(-0.154112736333057,-7.45225671948511E-5,0.175421172358873));
#17665=CARTESIAN_POINT('',(-0.1543,-1.01731279388251E-15,0.350421172358873));
#17666=CARTESIAN_POINT('Ctrl Pts',(-0.154112736333057,-7.45225671948471E-5,
0.175421172358873));
#17667=CARTESIAN_POINT('Ctrl Pts',(-0.153973346049181,0.0303998999070902,
0.173853938238567));
#17668=CARTESIAN_POINT('Ctrl Pts',(-0.130694151755309,0.111367805862998,
0.169700045481928));
#17669=CARTESIAN_POINT('Ctrl Pts',(-0.000871711368246156,0.181012066871201,
0.162959494088956));
#17670=CARTESIAN_POINT('Ctrl Pts',(0.149350085565286,0.102277888352765,
0.155199518179958));
#17671=CARTESIAN_POINT('Ctrl Pts',(0.168456255263351,-0.0662471829332422,
0.14743954227096));
#17672=CARTESIAN_POINT('Ctrl Pts',(0.0396733728729688,-0.17661315503135,
0.139679566361963));
#17673=CARTESIAN_POINT('Ctrl Pts',(-0.115072782317819,-0.134350623919955,
0.1323401097246));
#17674=CARTESIAN_POINT('Ctrl Pts',(-0.154056805498669,-0.041811035439686,
0.12758731172357));
#17675=CARTESIAN_POINT('Ctrl Pts',(-0.154397364694779,0.000110127730384357,
0.125421172358873));
#17676=CARTESIAN_POINT('Ctrl Pts',(-0.154326766555531,0.000123460234585825,
0.179578827641127));
#17677=CARTESIAN_POINT('Ctrl Pts',(-0.154418689716183,0.0108361910665024,
0.179025949336757));
#17678=CARTESIAN_POINT('Ctrl Pts',(-0.148597337680631,0.071569631208062,
0.175886412396054));
#17679=CARTESIAN_POINT('Ctrl Pts',(-0.0683530255288039,0.167611467503216,
0.170160216819019));
#17680=CARTESIAN_POINT('Ctrl Pts',(0.100397202365132,0.150621028353064,
0.162400240910021));
#17681=CARTESIAN_POINT('Ctrl Pts',(0.18100910679194,0.00139719974911195,
0.154640265001023));
#17682=CARTESIAN_POINT('Ctrl Pts',(0.102711092909207,-0.149052183789333,
0.146880289092025));
#17683=CARTESIAN_POINT('Ctrl Pts',(-0.0657574679958034,-0.168648048308422,
0.139120313183027));
#17684=CARTESIAN_POINT('Ctrl Pts',(-0.148058381688037,-0.0731761882111772,
0.133353159366061));
#17685=CARTESIAN_POINT('Ctrl Pts',(-0.154402705029802,-0.0116353181791797,
0.130172664185428));
#17686=CARTESIAN_POINT('Ctrl Pts',(-0.154304431028624,-0.000124889850439474,
0.129578827641127));
#17687=CARTESIAN_POINT('Origin',(0.,0.,0.350421172358873));
#17688=CARTESIAN_POINT('',(-0.154128406284035,-0.000157308197905263,0.229578827641128));
#17689=CARTESIAN_POINT('',(-0.154514081154978,3.38969080117728E-5,0.225421172358873));
#17690=CARTESIAN_POINT('',(-0.1543,-1.01731279388251E-15,0.350421172358873));
#17691=CARTESIAN_POINT('',(-0.0398513841857245,-0.149064942821851,0.24));
#17692=CARTESIAN_POINT('Ctrl Pts',(-0.0398513841857245,-0.149064942821851,
0.24));
#17693=CARTESIAN_POINT('Ctrl Pts',(-0.0883048112969314,-0.136111285829332,
0.237413341363667));
#17694=CARTESIAN_POINT('Ctrl Pts',(-0.143745772087175,-0.0847488633265083,
0.233939617244043));
#17695=CARTESIAN_POINT('Ctrl Pts',(-0.154234229255939,-0.017399338864059,
0.230465893124419));
#17696=CARTESIAN_POINT('Ctrl Pts',(-0.154128406284035,-0.00015730819790527,
0.229578827641128));
#17697=CARTESIAN_POINT('',(0.0399565498027962,-0.149273502906638,0.24));
#17698=CARTESIAN_POINT('Origin',(0.,0.,0.24));
#17699=CARTESIAN_POINT('Ctrl Pts',(0.0399565498027963,-0.149273502906638,
0.24));
#17700=CARTESIAN_POINT('Ctrl Pts',(-0.00490373130458673,-0.161043406468747,
0.237599759089979));
#17701=CARTESIAN_POINT('Ctrl Pts',(-0.107666111297752,-0.141562671532916,
0.23274014987627));
#17702=CARTESIAN_POINT('Ctrl Pts',(-0.154340128899266,-0.0474588267763927,
0.227880540662561));
#17703=CARTESIAN_POINT('Ctrl Pts',(-0.154514081154978,3.3896908011755E-5,
0.225421172358873));
#17704=CARTESIAN_POINT('Origin',(0.,0.,0.350421172358873));
#17705=CARTESIAN_POINT('Ctrl Pts',(-0.154514081154978,3.3896908011755E-5,
0.225421172358873));
#17706=CARTESIAN_POINT('Ctrl Pts',(-0.154523084458981,0.00249199339844659,
0.225293882026228));
#17707=CARTESIAN_POINT('Ctrl Pts',(-0.153375868586475,0.0548933889046004,
0.222579933057251));
#17708=CARTESIAN_POINT('Ctrl Pts',(-0.0942515706791253,0.154556313135293,
0.217279325451942));
#17709=CARTESIAN_POINT('Ctrl Pts',(0.0750450248431312,0.164716481511431,
0.209519349542944));
#17710=CARTESIAN_POINT('Ctrl Pts',(0.178461260043253,0.0303012077178856,
0.201759373633945));
#17711=CARTESIAN_POINT('Ctrl Pts',(0.125203781387627,-0.130731709675357,
0.193999397724948));
#17712=CARTESIAN_POINT('Ctrl Pts',(-0.0379704533096903,-0.17698585337688,
0.18623942181595));
#17713=CARTESIAN_POINT('Ctrl Pts',(-0.141587477595567,-0.0899051669249145,
0.180046680027258));
#17714=CARTESIAN_POINT('Ctrl Pts',(-0.154203404262525,-0.019896942829432,
0.176440596874899));
#17715=CARTESIAN_POINT('Ctrl Pts',(-0.154112736333057,-7.45225671948471E-5,
0.175421172358873));
#17716=CARTESIAN_POINT('Ctrl Pts',(-0.154128406284035,-0.00015730819790527,
0.229578827641128));
#17717=CARTESIAN_POINT('Ctrl Pts',(-0.153925652370292,0.0328779499839183,
0.227879234488086));
#17718=CARTESIAN_POINT('Ctrl Pts',(-0.127638532780061,0.116591914860373,
0.223592982698713));
#17719=CARTESIAN_POINT('Ctrl Pts',(0.00818767200092134,0.180778621679153,
0.216720072273006));
#17720=CARTESIAN_POINT('Ctrl Pts',(0.154249898498561,0.0947283641859207,
0.208960096364008));
#17721=CARTESIAN_POINT('Ctrl Pts',(0.164950538597243,-0.0745810526211722,
0.201200120455011));
#17722=CARTESIAN_POINT('Ctrl Pts',(0.0308106631569891,-0.178364693496558,
0.193440144546012));
#17723=CARTESIAN_POINT('Ctrl Pts',(-0.118879635670858,-0.129347344159377,
0.186233046941385));
#17724=CARTESIAN_POINT('Ctrl Pts',(-0.153988624301243,-0.0392836590090855,
0.18161260797309));
#17725=CARTESIAN_POINT('Ctrl Pts',(-0.154326766555531,0.000123460234585825,
0.179578827641127));
#17726=CARTESIAN_POINT('Ctrl Pts',(0.0958116152722397,0.0825211298936481,
0.24));
#17727=CARTESIAN_POINT('Ctrl Pts',(0.122635035163896,0.0513776495479799,
0.237413341363667));
#17728=CARTESIAN_POINT('Ctrl Pts',(0.143215100114593,-0.0385359791949074,
0.232240024091002));
#17729=CARTESIAN_POINT('Ctrl Pts',(0.0482740424593604,-0.140360024672886,
0.224480048182004));
#17730=CARTESIAN_POINT('Ctrl Pts',(-0.0890179591196291,-0.118613269413641,
0.216720072273006));
#17731=CARTESIAN_POINT('Ctrl Pts',(-0.148173729266643,0.00709031985706173,
0.208960096364008));
#17732=CARTESIAN_POINT('Ctrl Pts',(-0.0772398646297824,0.126660050524678,
0.20120012045501));
#17733=CARTESIAN_POINT('Ctrl Pts',(0.0614999571705377,0.134986384232796,
0.193440144546013));
#17734=CARTESIAN_POINT('Ctrl Pts',(0.146250332679645,0.0248320655601208,
0.185680168637014));
#17735=CARTESIAN_POINT('Ctrl Pts',(0.102605431992647,-0.107135610424167,
0.177920192728017));
#17736=CARTESIAN_POINT('Ctrl Pts',(-0.0311170694815965,-0.145041225920327,
0.170160216819019));
#17737=CARTESIAN_POINT('Ctrl Pts',(-0.137521919612742,-0.0556176253575994,
0.162400240910021));
#17738=CARTESIAN_POINT('Ctrl Pts',(-0.123195064154356,0.0826350160503635,
0.154640265001023));
#17739=CARTESIAN_POINT('Ctrl Pts',(-0.000714373963154436,0.148340737886347,
0.146880289092025));
#17740=CARTESIAN_POINT('Ctrl Pts',(0.122393508228972,0.0838174917835845,
0.139120313183027));
#17741=CARTESIAN_POINT('Ctrl Pts',(0.138051156695079,-0.0542900601549481,
0.131360337274029));
#17742=CARTESIAN_POINT('Ctrl Pts',(0.032512624755586,-0.14473579684844,
0.123600361365031));
#17743=CARTESIAN_POINT('Ctrl Pts',(-0.101568992309399,-0.108116932194331,
0.115840385456033));
#17744=CARTESIAN_POINT('Ctrl Pts',(-0.146482409833755,0.0234186855983926,
0.108080409547036));
#17745=CARTESIAN_POINT('Ctrl Pts',(-0.0627977522708403,0.13439480632666,
0.100320433638038));
#17746=CARTESIAN_POINT('Ctrl Pts',(0.076017492057093,0.127384745546031,
0.0925604577290397));
#17747=CARTESIAN_POINT('Ctrl Pts',(0.148096483096158,0.00854251017184644,
0.0848004818200417));
#17748=CARTESIAN_POINT('Ctrl Pts',(0.0901602332714121,-0.117799054254564,
0.0770405059110438));
#17749=CARTESIAN_POINT('Ctrl Pts',(-0.0469280390901857,-0.140724300875114,
0.069280530002046));
#17750=CARTESIAN_POINT('Ctrl Pts',(-0.142818485852497,-0.0401058440029853,
0.0615205540930479));
#17751=CARTESIAN_POINT('Ctrl Pts',(-0.113326201176411,0.0957204333280909,
0.0537605781840501));
#17752=CARTESIAN_POINT('Ctrl Pts',(0.0156536221268617,0.147515686656254,
0.0460006022750521));
#17753=CARTESIAN_POINT('Ctrl Pts',(0.130895613795878,0.0698006416724775,
0.0382406263660543));
#17754=CARTESIAN_POINT('Ctrl Pts',(0.13121455111358,-0.0691831643991777,
0.0304806504570563));
#17755=CARTESIAN_POINT('Ctrl Pts',(0.0163559286405278,-0.147449139316739,
0.0227206745480584));
#17756=CARTESIAN_POINT('Ctrl Pts',(-0.112893560070904,-0.0962328986104914,
0.0149606986390606));
#17757=CARTESIAN_POINT('Ctrl Pts',(-0.142972035491037,0.0393992613429074,
0.00720072273006258));
#17758=CARTESIAN_POINT('Ctrl Pts',(-0.0476516261894416,0.140572551456688,
-0.000559253178935252));
#17759=CARTESIAN_POINT('Ctrl Pts',(0.0897382482543901,0.118078928660352,
-0.00831922908793326));
#17760=CARTESIAN_POINT('Ctrl Pts',(0.128447313976429,0.0343555272840613,
-0.0134925463605985));
#17761=CARTESIAN_POINT('Ctrl Pts',(0.126272937371016,-0.00668937872268922,
-0.0160792049969311));
#17762=CARTESIAN_POINT('Ctrl Pts',(0.102845629995666,0.0885794229410663,
0.245359734998977));
#17763=CARTESIAN_POINT('Ctrl Pts',(0.13163829265517,0.0551495423644061,
0.242773076362644));
#17764=CARTESIAN_POINT('Ctrl Pts',(0.153729244145676,-0.0413651001137901,
0.237599759089979));
#17765=CARTESIAN_POINT('Ctrl Pts',(0.0518180837997932,-0.150664563191773,
0.229839783180981));
#17766=CARTESIAN_POINT('Ctrl Pts',(-0.0955532172229155,-0.127321268762976,
0.222079807271983));
#17767=CARTESIAN_POINT('Ctrl Pts',(-0.159051911315084,0.00761085605850937,
0.214319831362985));
#17768=CARTESIAN_POINT('Ctrl Pts',(-0.0829104333128967,0.135958804728216,
0.206559855453988));
#17769=CARTESIAN_POINT('Ctrl Pts',(0.0660149797280689,0.144896416659008,
0.19879987954499));
#17770=CARTESIAN_POINT('Ctrl Pts',(0.156987308467515,0.0266551129460425,
0.191039903635992));
#17771=CARTESIAN_POINT('Ctrl Pts',(0.110138215124307,-0.11500097684123,
0.183279927726994));
#17772=CARTESIAN_POINT('Ctrl Pts',(-0.0334015307576278,-0.155689435072511,
0.175519951817996));
#17773=CARTESIAN_POINT('Ctrl Pts',(-0.147618098500879,-0.0597007962188336,
0.167759975908998));
#17774=CARTESIAN_POINT('Ctrl Pts',(-0.13223943620312,0.0887016700559064,
0.16));
#17775=CARTESIAN_POINT('Ctrl Pts',(-0.000766819764851659,0.159231180881298,
0.152240024091002));
#17776=CARTESIAN_POINT('Ctrl Pts',(0.131379034007743,0.0899709573066447,
0.144480048182004));
#17777=CARTESIAN_POINT('Ctrl Pts',(0.14818618955117,-0.0582757677477129,
0.136720072273006));
#17778=CARTESIAN_POINT('Ctrl Pts',(0.0348995407947136,-0.15536158290941,
0.128960096364009));
#17779=CARTESIAN_POINT('Ctrl Pts',(-0.109025685167754,-0.116054342400242,
0.12120012045501));
#17780=CARTESIAN_POINT('Ctrl Pts',(-0.157236423577976,0.0251379696208395,
0.113440144546013));
#17781=CARTESIAN_POINT('Ctrl Pts',(-0.0674080525232269,0.144261408030094,
0.105680168637014));
#17782=CARTESIAN_POINT('Ctrl Pts',(0.0815983201941432,0.136736703272292,
0.0979201927280168));
#17783=CARTESIAN_POINT('Ctrl Pts',(0.158968994112971,0.00916965900085902,
0.0901602168190187));
#17784=CARTESIAN_POINT('Ctrl Pts',(0.0967793514910216,-0.126447277955604,
0.0824002409100209));
#17785=CARTESIAN_POINT('Ctrl Pts',(-0.0503732635231939,-0.151055582750353,
0.0746402650010229));
#17786=CARTESIAN_POINT('Ctrl Pts',(-0.15330351242688,-0.0430502166284845,
0.066880289092025));
#17787=CARTESIAN_POINT('Ctrl Pts',(-0.121646050135849,0.102747753924341,
0.0591203131830272));
#17788=CARTESIAN_POINT('Ctrl Pts',(0.0168028336102756,0.158345558472194,
0.0513603372740292));
#17789=CARTESIAN_POINT('Ctrl Pts',(0.140505322097486,0.074925059414875,
0.0436003613650313));
#17790=CARTESIAN_POINT('Ctrl Pts',(0.140847674214973,-0.0742622500154084,
0.0358403854560334));
#17791=CARTESIAN_POINT('Ctrl Pts',(0.0175566999932067,-0.158274125556283,
0.0280804095470355));
#17792=CARTESIAN_POINT('Ctrl Pts',(-0.121181646661057,-0.103297841872129,
0.0203204336380376));
#17793=CARTESIAN_POINT('Ctrl Pts',(-0.153468334920127,0.0422917601656304,
0.0125604577290396));
#17794=CARTESIAN_POINT('Ctrl Pts',(-0.0511499728070136,0.150892692640473,
0.00480048182004178));
#17795=CARTESIAN_POINT('Ctrl Pts',(0.0963263864220051,0.126747699355464,
-0.00295949408895622));
#17796=CARTESIAN_POINT('Ctrl Pts',(0.137877280219327,0.0368777401082635,
-0.00813281136162143));
#17797=CARTESIAN_POINT('Ctrl Pts',(0.135543271642224,-0.00718047980988283,
-0.0107194699979541));
#17798=CARTESIAN_POINT('Ctrl Pts',(0.109879644719093,0.0946377159884845,
0.250719469997954));
#17799=CARTESIAN_POINT('Ctrl Pts',(0.140641550146443,0.0589214351808321,
0.248132811361621));
#17800=CARTESIAN_POINT('Ctrl Pts',(0.164243388176759,-0.0441942210326729,
0.242959494088956));
#17801=CARTESIAN_POINT('Ctrl Pts',(0.055362125140226,-0.160969101710661,
0.235199518179958));
#17802=CARTESIAN_POINT('Ctrl Pts',(-0.102088475326202,-0.13602926811231,
0.227439542270961));
#17803=CARTESIAN_POINT('Ctrl Pts',(-0.169930093363525,0.00813139225995705,
0.219679566361962));
#17804=CARTESIAN_POINT('Ctrl Pts',(-0.0885810019960112,0.145257558931755,
0.211919590452965));
#17805=CARTESIAN_POINT('Ctrl Pts',(0.0705300022856002,0.154806449085219,
0.204159614543967));
#17806=CARTESIAN_POINT('Ctrl Pts',(0.167724284255384,0.0284781603319641,
0.196399638634969));
#17807=CARTESIAN_POINT('Ctrl Pts',(0.117670998255967,-0.122866343258294,
0.188639662725971));
#17808=CARTESIAN_POINT('Ctrl Pts',(-0.0356859920336591,-0.166337644224695,
0.180879686816973));
#17809=CARTESIAN_POINT('Ctrl Pts',(-0.157714277389017,-0.0637839670800676,
0.173119710907975));
#17810=CARTESIAN_POINT('Ctrl Pts',(-0.141283808251885,0.0947683240614489,
0.165359734998977));
#17811=CARTESIAN_POINT('Ctrl Pts',(-0.000819265566548849,0.17012162387625,
0.157599759089979));
#17812=CARTESIAN_POINT('Ctrl Pts',(0.140364559786514,0.0961244228297045,
0.149839783180981));
#17813=CARTESIAN_POINT('Ctrl Pts',(0.158321222407261,-0.0622614753404775,
0.142079807271983));
#17814=CARTESIAN_POINT('Ctrl Pts',(0.0372864568338413,-0.16598736897038,
0.134319831362986));
#17815=CARTESIAN_POINT('Ctrl Pts',(-0.116482378026109,-0.123991752606152,
0.126559855453987));
#17816=CARTESIAN_POINT('Ctrl Pts',(-0.167990437322196,0.0268572536432864,
0.11879987954499));
#17817=CARTESIAN_POINT('Ctrl Pts',(-0.0720183527756138,0.154128009733527,
0.111039903635992));
#17818=CARTESIAN_POINT('Ctrl Pts',(0.0871791483311938,0.146088660998552,
0.103279927726994));
#17819=CARTESIAN_POINT('Ctrl Pts',(0.169841505129784,0.00979680782987164,
0.0955199518179957));
#17820=CARTESIAN_POINT('Ctrl Pts',(0.103398469710631,-0.135095501656644,
0.0877599759089979));
#17821=CARTESIAN_POINT('Ctrl Pts',(-0.0538184879562023,-0.161386864625592,
0.08));
#17822=CARTESIAN_POINT('Ctrl Pts',(-0.163788539001263,-0.0459945892539838,
0.0722400240910021));
#17823=CARTESIAN_POINT('Ctrl Pts',(-0.129965899095288,0.10977507452059,
0.0644800481820042));
#17824=CARTESIAN_POINT('Ctrl Pts',(0.0179520450936897,0.169175430288133,
0.0567200722730062));
#17825=CARTESIAN_POINT('Ctrl Pts',(0.150115030399095,0.0800494771572726,
0.0489600963640084));
#17826=CARTESIAN_POINT('Ctrl Pts',(0.150480797316365,-0.0793413356316391,
0.0412001204550104));
#17827=CARTESIAN_POINT('Ctrl Pts',(0.0187574713458855,-0.169099111795828,
0.0334401445460125));
#17828=CARTESIAN_POINT('Ctrl Pts',(-0.129469733251211,-0.110362785133767,
0.0256801686370146));
#17829=CARTESIAN_POINT('Ctrl Pts',(-0.163964634349217,0.0451842589883535,
0.0179201927280167));
#17830=CARTESIAN_POINT('Ctrl Pts',(-0.0546483194245858,0.161212833824257,
0.0101602168190188));
#17831=CARTESIAN_POINT('Ctrl Pts',(0.10291452458962,0.135416470050577,0.00240024091002082));
#17832=CARTESIAN_POINT('Ctrl Pts',(0.147307246462226,0.0393999529324658,
-0.00277307636264439));
#17833=CARTESIAN_POINT('Ctrl Pts',(0.144813605913432,-0.00767158089707644,
-0.00535973499897704));
#17834=CARTESIAN_POINT('Ctrl Pts',(0.116913659442519,0.100696009035903,
0.256079204996931));
#17835=CARTESIAN_POINT('Ctrl Pts',(0.149644807637716,0.0626933279972582,
0.253492546360598));
#17836=CARTESIAN_POINT('Ctrl Pts',(0.174757532207842,-0.0470233419515556,
0.248319229087933));
#17837=CARTESIAN_POINT('Ctrl Pts',(0.0589061664806588,-0.171273640229548,
0.240559253178935));
#17838=CARTESIAN_POINT('Ctrl Pts',(-0.108623733429488,-0.144737267461644,
0.232799277269938));
#17839=CARTESIAN_POINT('Ctrl Pts',(-0.180808275411966,0.00865192846140473,
0.225039301360939));
#17840=CARTESIAN_POINT('Ctrl Pts',(-0.0942515706791253,0.154556313135293,
0.217279325451942));
#17841=CARTESIAN_POINT('Ctrl Pts',(0.0750450248431312,0.164716481511431,
0.209519349542944));
#17842=CARTESIAN_POINT('Ctrl Pts',(0.178461260043253,0.0303012077178856,
0.201759373633945));
#17843=CARTESIAN_POINT('Ctrl Pts',(0.125203781387627,-0.130731709675357,
0.193999397724948));
#17844=CARTESIAN_POINT('Ctrl Pts',(-0.0379704533096903,-0.17698585337688,
0.18623942181595));
#17845=CARTESIAN_POINT('Ctrl Pts',(-0.167810456277154,-0.0678671379413016,
0.178479445906952));
#17846=CARTESIAN_POINT('Ctrl Pts',(-0.150328180300649,0.100834978066992,
0.170719469997954));
#17847=CARTESIAN_POINT('Ctrl Pts',(-0.000871711368246156,0.181012066871201,
0.162959494088956));
#17848=CARTESIAN_POINT('Ctrl Pts',(0.149350085565286,0.102277888352765,
0.155199518179958));
#17849=CARTESIAN_POINT('Ctrl Pts',(0.168456255263351,-0.0662471829332422,
0.14743954227096));
#17850=CARTESIAN_POINT('Ctrl Pts',(0.0396733728729688,-0.17661315503135,
0.139679566361963));
#17851=CARTESIAN_POINT('Ctrl Pts',(-0.123939070884463,-0.131929162812062,
0.131919590452964));
#17852=CARTESIAN_POINT('Ctrl Pts',(-0.178744451066417,0.0285765376657333,
0.124159614543967));
#17853=CARTESIAN_POINT('Ctrl Pts',(-0.0766286530280003,0.163994611436961,
0.116399638634969));
#17854=CARTESIAN_POINT('Ctrl Pts',(0.0927599764682439,0.155440618724813,
0.108639662725971));
#17855=CARTESIAN_POINT('Ctrl Pts',(0.180714016146597,0.0104239566588842,
0.100879686816973));
#17856=CARTESIAN_POINT('Ctrl Pts',(0.11001758793024,-0.143743725357685,
0.093119710907975));
#17857=CARTESIAN_POINT('Ctrl Pts',(-0.0572637123892103,-0.171718146500831,
0.0853597349989769));
#17858=CARTESIAN_POINT('Ctrl Pts',(-0.174273565575645,-0.048938961879483,
0.0775997590899791));
#17859=CARTESIAN_POINT('Ctrl Pts',(-0.138285748054726,0.11680239511684,
0.0698397831809812));
#17860=CARTESIAN_POINT('Ctrl Pts',(0.0191012565771036,0.180005302104073,
0.0620798072719832));
#17861=CARTESIAN_POINT('Ctrl Pts',(0.159724738700703,0.0851738948996701,
0.0543198313629854));
#17862=CARTESIAN_POINT('Ctrl Pts',(0.160113920417758,-0.0844204212478698,
0.0465598554539874));
#17863=CARTESIAN_POINT('Ctrl Pts',(0.0199582426985643,-0.179924098035372,
0.0387998795449896));
#17864=CARTESIAN_POINT('Ctrl Pts',(-0.137757819841364,-0.117427728395404,
0.0310399036359917));
#17865=CARTESIAN_POINT('Ctrl Pts',(-0.174460933778308,0.0480767578110765,
0.0232799277269937));
#17866=CARTESIAN_POINT('Ctrl Pts',(-0.0581466660421577,0.171532975008042,
0.0155199518179959));
#17867=CARTESIAN_POINT('Ctrl Pts',(0.109502662757235,0.144085240745689,
0.00775997590899784));
#17868=CARTESIAN_POINT('Ctrl Pts',(0.156737212705124,0.0419221657566679,
0.00258665863633264));
#17869=CARTESIAN_POINT('Ctrl Pts',(0.15408394018464,-0.00816268198427004,
0.));
#17870=CARTESIAN_POINT('Ctrl Pts',(0.15408394018464,-0.00816268198427004,
0.));
#17871=CARTESIAN_POINT('Ctrl Pts',(0.153697863146473,0.00250812953454787,
1.45220469349306E-17));
#17872=CARTESIAN_POINT('Ctrl Pts',(0.152123106309386,0.0130673133993916,
-2.32988231788825E-17));
#17873=CARTESIAN_POINT('Ctrl Pts',(0.149466152202855,0.0233620190894148,
-6.07153216591882E-17));
#17874=CARTESIAN_POINT('Ctrl Pts',(0.14793019248835,0.0293132898222067,
-8.23454409684948E-17));
#17875=CARTESIAN_POINT('Ctrl Pts',(0.146031563681721,0.0351760135160456,
3.17823908273165E-17));
#17876=CARTESIAN_POINT('Ctrl Pts',(0.143784059453749,0.0409171473780902,
6.24500451351651E-17));
#17877=CARTESIAN_POINT('Ctrl Pts',(0.142595904075608,0.0439522291322952,
7.86626679846993E-17));
#17878=CARTESIAN_POINT('Ctrl Pts',(0.141309213132582,0.0469553015723855,
1.03399090950918E-16));
#17879=CARTESIAN_POINT('Ctrl Pts',(0.13992871365498,0.0499144025840292,
1.00613961606655E-16));
#17880=CARTESIAN_POINT('Ctrl Pts',(0.135493978469587,0.0594202586791481,
9.16669744478229E-17));
#17881=CARTESIAN_POINT('Ctrl Pts',(0.130119641392827,0.0684241765595774,
5.76730757846686E-17));
#17882=CARTESIAN_POINT('Ctrl Pts',(0.123887660540245,0.0767683201192124,
1.38777878078145E-16));
#17883=CARTESIAN_POINT('Ctrl Pts',(0.120656388342022,0.0810947453345699,
1.808305895663E-16));
#17884=CARTESIAN_POINT('Ctrl Pts',(0.117193874983239,0.0852432898306738,
1.062697842984E-16));
#17885=CARTESIAN_POINT('Ctrl Pts',(0.11350808038867,0.0891875047540603,
1.14491749414469E-16));
#17886=CARTESIAN_POINT('Ctrl Pts',(0.110158526423333,0.0927719043720516,
1.21963656801269E-16));
#17887=CARTESIAN_POINT('Ctrl Pts',(0.106618991420749,0.0961915975683434,
1.17223950247179E-16));
#17888=CARTESIAN_POINT('Ctrl Pts',(0.102922970874274,0.0994011657423757,
1.02348685082632E-16));
#17889=CARTESIAN_POINT('Ctrl Pts',(0.0973787571548163,0.104215676830788,
8.00350512245867E-17));
#17890=CARTESIAN_POINT('Ctrl Pts',(0.0914754811895955,0.108568278221023,
6.56075743842472E-17));
#17891=CARTESIAN_POINT('Ctrl Pts',(0.0852365492443714,0.11239450959967,
3.29597460435593E-17));
#17892=CARTESIAN_POINT('Ctrl Pts',(0.0787787796913796,0.116354950379705,
-7.26807264206779E-19));
#17893=CARTESIAN_POINT('Ctrl Pts',(0.0719608771003193,0.11975150351845,
7.81983513604452E-17));
#17894=CARTESIAN_POINT('Ctrl Pts',(0.0648645680501024,0.122569786811788,
1.05818132034585E-16));
#17895=CARTESIAN_POINT('Ctrl Pts',(0.0619760396963809,0.123716959397427,
1.17060669392563E-16));
#17896=CARTESIAN_POINT('Ctrl Pts',(0.0590419697559043,0.124767587801255,
-1.70921410850511E-17));
#17897=CARTESIAN_POINT('Ctrl Pts',(0.0560804949635964,0.12571697313192,
-8.67361737988404E-19));
#17898=CARTESIAN_POINT('Ctrl Pts',(0.0481895916857994,0.128246627558523,
4.23638569993146E-17));
#17899=CARTESIAN_POINT('Ctrl Pts',(0.040081547172159,0.13006877931966,2.48189907303608E-17));
#17900=CARTESIAN_POINT('Ctrl Pts',(0.0318655688619291,0.131172622122806,
0.));
#17901=CARTESIAN_POINT('Ctrl Pts',(0.0267717292715239,0.131856995664207,
-1.5387571972871E-17));
#17902=CARTESIAN_POINT('Ctrl Pts',(0.0216363184326117,0.132264755542675,
5.61228976213782E-17));
#17903=CARTESIAN_POINT('Ctrl Pts',(0.0164863123329273,0.132388468809724,
3.03576608295941E-17));
#17904=CARTESIAN_POINT('Ctrl Pts',(0.0120733572364389,0.13249447666326,
8.27985532573229E-18));
#17905=CARTESIAN_POINT('Ctrl Pts',(0.00764667637530932,0.132391154756805,
7.9933444120104E-17));
#17906=CARTESIAN_POINT('Ctrl Pts',(0.00324855819595315,0.132074892239241,
9.62771529167128E-17));
#17907=CARTESIAN_POINT('Ctrl Pts',(-0.00215998367955725,0.131685971569047,
1.16375665467493E-16));
#17908=CARTESIAN_POINT('Ctrl Pts',(-0.00753310453775717,0.130975837616781,
1.12286849362194E-16));
#17909=CARTESIAN_POINT('Ctrl Pts',(-0.0128378223015392,0.129936202211006,
1.27068494615301E-16));
#17910=CARTESIAN_POINT('Ctrl Pts',(-0.0180922709275414,0.128906418710228,
1.41710064449709E-16));
#17911=CARTESIAN_POINT('Ctrl Pts',(-0.023283936630727,0.12755123862641,
1.19281234835921E-16));
#17912=CARTESIAN_POINT('Ctrl Pts',(-0.028350637156304,0.125868914531291,
9.19403442267708E-17));
#17913=CARTESIAN_POINT('Ctrl Pts',(-0.0326437071621008,0.124443463179602,
6.87741127091605E-17));
#17914=CARTESIAN_POINT('Ctrl Pts',(-0.0368509055758185,0.122782751372096,
3.08039683582783E-17));
#17915=CARTESIAN_POINT('Ctrl Pts',(-0.0409513668396969,0.120880349084932,
-1.95156391047391E-18));
#17916=CARTESIAN_POINT('Ctrl Pts',(-0.0436523616789034,0.119627226953286,
-2.45035827619675E-17));
#17917=CARTESIAN_POINT('Ctrl Pts',(-0.0463070048384274,0.118269169850402,
-4.56986185075063E-18));
#17918=CARTESIAN_POINT('Ctrl Pts',(-0.0489111879062984,0.116810626195002,
-1.73472347597681E-18));
#17919=CARTESIAN_POINT('Ctrl Pts',(0.0958116152722397,0.0825211298936481,
0.24));
#17920=CARTESIAN_POINT('Ctrl Pts',(0.102494250906434,0.0762804363331629,
0.24));
#17921=CARTESIAN_POINT('Ctrl Pts',(0.108399952301676,0.0693089192431419,
0.24));
#17922=CARTESIAN_POINT('Ctrl Pts',(0.113520383394708,0.0617855200816623,
0.24));
#17923=CARTESIAN_POINT('Ctrl Pts',(0.11760088593285,0.0557900777417299,
0.24));
#17924=CARTESIAN_POINT('Ctrl Pts',(0.1211824537664,0.0494427873910869,0.24));
#17925=CARTESIAN_POINT('Ctrl Pts',(0.124247292533427,0.0428169095598754,
0.24));
#17926=CARTESIAN_POINT('Ctrl Pts',(0.125635784531567,0.0398151273949318,
0.24));
#17927=CARTESIAN_POINT('Ctrl Pts',(0.126914357096627,0.0367636074968772,
0.24));
#17928=CARTESIAN_POINT('Ctrl Pts',(0.128080244072735,0.0336751552254939,
0.24));
#17929=CARTESIAN_POINT('Ctrl Pts',(0.13155694143068,0.024465331227027,0.24));
#17930=CARTESIAN_POINT('Ctrl Pts',(0.134041462136676,0.0149150332268467,
0.24));
#17931=CARTESIAN_POINT('Ctrl Pts',(0.135496608205084,0.00520422800883078,
0.24));
#17932=CARTESIAN_POINT('Ctrl Pts',(0.136052940597398,0.00149158663520877,
0.24));
#17933=CARTESIAN_POINT('Ctrl Pts',(0.136458356591543,-0.00224482315054724,
0.24));
#17934=CARTESIAN_POINT('Ctrl Pts',(0.136708928272429,-0.00599574054845843,
0.24));
#17935=CARTESIAN_POINT('Ctrl Pts',(0.136894600108428,-0.00877514370161729,
0.24));
#17936=CARTESIAN_POINT('Ctrl Pts',(0.136994942037659,-0.0115613689854128,
0.24));
#17937=CARTESIAN_POINT('Ctrl Pts',(0.137008733057845,-0.0143405417274864,
0.24));
#17938=CARTESIAN_POINT('Ctrl Pts',(0.137045731231951,-0.0217964308202384,
0.24));
#17939=CARTESIAN_POINT('Ctrl Pts',(0.136462408227525,-0.0292204075226799,
0.24));
#17940=CARTESIAN_POINT('Ctrl Pts',(0.135240454646173,-0.0365388974416549,
0.24));
#17941=CARTESIAN_POINT('Ctrl Pts',(0.134058793448489,-0.0436160693529878,
0.24));
#17942=CARTESIAN_POINT('Ctrl Pts',(0.132280018312676,-0.050595007513092,
0.24));
#17943=CARTESIAN_POINT('Ctrl Pts',(0.129952822193542,-0.0574290655609092,
0.24));
#17944=CARTESIAN_POINT('Ctrl Pts',(0.128850070284018,-0.0606674134165377,
0.24));
#17945=CARTESIAN_POINT('Ctrl Pts',(0.127623182384127,-0.0638741644409745,
0.24));
#17946=CARTESIAN_POINT('Ctrl Pts',(0.126284110088584,-0.067028198101918,
0.24));
#17947=CARTESIAN_POINT('Ctrl Pts',(0.122654675969015,-0.0755769205431157,
0.24));
#17948=CARTESIAN_POINT('Ctrl Pts',(0.118195290975453,-0.0837663478860722,
0.24));
#17949=CARTESIAN_POINT('Ctrl Pts',(0.113014989178579,-0.0915013065162071,
0.24));
#17950=CARTESIAN_POINT('Ctrl Pts',(0.108985931714537,-0.0975172866704144,
0.24));
#17951=CARTESIAN_POINT('Ctrl Pts',(0.104519884911976,-0.103258562704539,
0.24));
#17952=CARTESIAN_POINT('Ctrl Pts',(0.0996546828651377,-0.108675969178894,
0.24));
#17953=CARTESIAN_POINT('Ctrl Pts',(0.0972822643803542,-0.11131765910988,
0.24));
#17954=CARTESIAN_POINT('Ctrl Pts',(0.09482095240722,-0.113875293456495,
0.24));
#17955=CARTESIAN_POINT('Ctrl Pts',(0.0922773332174137,-0.116342466058553,
0.24));
#17956=CARTESIAN_POINT('Ctrl Pts',(0.0868426048671788,-0.121613857680014,
0.24));
#17957=CARTESIAN_POINT('Ctrl Pts',(0.0810310485854155,-0.126474759557936,
0.24));
#17958=CARTESIAN_POINT('Ctrl Pts',(0.0748870600798396,-0.130870957562724,
0.24));
#17959=CARTESIAN_POINT('Ctrl Pts',(0.0715378781224404,-0.133267392228159,
0.24));
#17960=CARTESIAN_POINT('Ctrl Pts',(0.0680912231566627,-0.135524142754832,
0.24));
#17961=CARTESIAN_POINT('Ctrl Pts',(0.0645638484115253,-0.13762659390894,
0.24));
#17962=CARTESIAN_POINT('Ctrl Pts',(0.0598451535113139,-0.140439117742,0.24));
#17963=CARTESIAN_POINT('Ctrl Pts',(0.0549775790306604,-0.142978967531553,
0.24));
#17964=CARTESIAN_POINT('Ctrl Pts',(0.0499773507040556,-0.145225083935062,
0.24));
#17965=CARTESIAN_POINT('Ctrl Pts',(0.0466920976074369,-0.146700828718701,
0.24));
#17966=CARTESIAN_POINT('Ctrl Pts',(0.0433495270099635,-0.148049731670784,
0.24));
#17967=CARTESIAN_POINT('Ctrl Pts',(0.039956549802796,-0.149273502906639,
0.24));
#17968=CARTESIAN_POINT('Ctrl Pts',(-0.126296536029262,-6.10717992316628E-5,
0.159341967361942));
#17969=CARTESIAN_POINT('Ctrl Pts',(-0.12637083907321,-0.0163056929409037,
0.160361391877968));
#17970=CARTESIAN_POINT('Ctrl Pts',(-0.12344809088261,-0.0325245895549842,
0.161380816393994));
#17971=CARTESIAN_POINT('Ctrl Pts',(-0.117399968681154,-0.0474794518833934,
0.162400240910021));
#17972=CARTESIAN_POINT('Ctrl Pts',(-0.102053636235694,-0.0854254922118417,
0.164986899546353));
#17973=CARTESIAN_POINT('Ctrl Pts',(-0.0665853528586453,-0.115233359066084,
0.167573558182686));
#17974=CARTESIAN_POINT('Ctrl Pts',(-0.0265641275910804,-0.123819689910512,
0.170160216819019));
#17975=CARTESIAN_POINT('Ctrl Pts',(0.0134570976764845,-0.13240602075494,
0.172746875455351));
#17976=CARTESIAN_POINT('Ctrl Pts',(0.058031264834566,-0.119770815589554,
0.175333534091684));
#17977=CARTESIAN_POINT('Ctrl Pts',(0.0875924985281064,-0.0914586003428122,
0.177920192728017));
#17978=CARTESIAN_POINT('Ctrl Pts',(0.117153732221647,-0.0631463850960709,
0.180506851364349));
#17979=CARTESIAN_POINT('Ctrl Pts',(0.131702032450646,-0.0191571597679751,
0.183093510000682));
#17980=CARTESIAN_POINT('Ctrl Pts',(0.124851119980295,0.0211965060081854,
0.185680168637015));
#17981=CARTESIAN_POINT('Ctrl Pts',(0.118000207509943,0.0615501717843459,
0.188266827273347));
#17982=CARTESIAN_POINT('Ctrl Pts',(0.0897500823402403,0.0982682780085711,
0.19085348590968));
#17983=CARTESIAN_POINT('Ctrl Pts',(0.0525017161220023,0.115239608835997,
0.193440144546013));
#17984=CARTESIAN_POINT('Ctrl Pts',(0.0152533499037644,0.132210939663423,
0.196026803182345));
#17985=CARTESIAN_POINT('Ctrl Pts',(-0.030993257363009,0.129435495094051,
0.198613461818678));
#17986=CARTESIAN_POINT('Ctrl Pts',(-0.0659388717692058,0.108119484364762,
0.20120012045501));
#17987=CARTESIAN_POINT('Ctrl Pts',(-0.100884486175403,0.0868034736354726,
0.203786779091343));
#17988=CARTESIAN_POINT('Ctrl Pts',(-0.124529107721023,0.0469468967462671,
0.206373437727676));
#17989=CARTESIAN_POINT('Ctrl Pts',(-0.126492123469331,0.00606801008988057,
0.208960096364008));
#17990=CARTESIAN_POINT('Ctrl Pts',(-0.126588724127832,0.00405634646811867,
0.209087386696653));
#17991=CARTESIAN_POINT('Ctrl Pts',(-0.126632819376787,0.00204220716288977,
0.209214677029297));
#17992=CARTESIAN_POINT('Ctrl Pts',(-0.126625441102054,2.7778768752873E-5,
0.209341967361942));
#17993=CARTESIAN_POINT('Ctrl Pts',(-0.0398513841857245,-0.149064942821851,
0.24));
#17994=CARTESIAN_POINT('Ctrl Pts',(-0.0883048112969314,-0.136111285829332,
0.237413341363667));
#17995=CARTESIAN_POINT('Ctrl Pts',(-0.170871437255804,-0.0596187094618861,
0.232240024091002));
#17996=CARTESIAN_POINT('Ctrl Pts',(-0.145169204726118,0.108307533342445,
0.224480048182004));
#17997=CARTESIAN_POINT('Ctrl Pts',(0.00818767200092134,0.180778621679153,
0.216720072273006));
#17998=CARTESIAN_POINT('Ctrl Pts',(0.154249898498561,0.0947283641859207,
0.208960096364008));
#17999=CARTESIAN_POINT('Ctrl Pts',(0.164950538597243,-0.0745810526211722,
0.201200120455011));
#18000=CARTESIAN_POINT('Ctrl Pts',(0.0308106631569891,-0.178364693496558,
0.193440144546012));
#18001=CARTESIAN_POINT('Ctrl Pts',(-0.13036283225522,-0.125587074703769,
0.185680168637015));
#18002=CARTESIAN_POINT('Ctrl Pts',(-0.17709781441264,0.03745832727601,0.177920192728017));
#18003=CARTESIAN_POINT('Ctrl Pts',(-0.0683530255288039,0.167611467503216,
0.170160216819019));
#18004=CARTESIAN_POINT('Ctrl Pts',(0.100397202365132,0.150621028353064,
0.162400240910021));
#18005=CARTESIAN_POINT('Ctrl Pts',(0.18100910679194,0.00139719974911195,
0.154640265001023));
#18006=CARTESIAN_POINT('Ctrl Pts',(0.102711092909207,-0.149052183789333,
0.146880289092025));
#18007=CARTESIAN_POINT('Ctrl Pts',(-0.0657574679958034,-0.168648048308422,
0.139120313183027));
#18008=CARTESIAN_POINT('Ctrl Pts',(-0.176497206835689,-0.0401861834345609,
0.131360337274029));
#18009=CARTESIAN_POINT('Ctrl Pts',(-0.132288575936487,0.123555290563421,
0.123600361365031));
#18010=CARTESIAN_POINT('Ctrl Pts',(0.0280571680938306,0.178826694862324,
0.115840385456033));
#18011=CARTESIAN_POINT('Ctrl Pts',(0.163771354656592,0.0771047007047774,
0.108080409547035));
#18012=CARTESIAN_POINT('Ctrl Pts',(0.155709331479018,-0.0923080778690166,
0.100320433638038));
#18013=CARTESIAN_POINT('Ctrl Pts',(0.0109489686262093,-0.180682908560435,
0.0925604577290397));
#18014=CARTESIAN_POINT('Ctrl Pts',(-0.143423754439364,-0.110434756566834,
0.0848004818200417));
#18015=CARTESIAN_POINT('Ctrl Pts',(-0.17188331593326,0.0567648465404429,
0.0770405059110439));
#18016=CARTESIAN_POINT('Ctrl Pts',(-0.0494457976037486,0.174130301808973,
0.0692805300020459));
#18017=CARTESIAN_POINT('Ctrl Pts',(0.11640175885633,0.13862511662766,0.061520554093048));
#18018=CARTESIAN_POINT('Ctrl Pts',(0.18005704388064,-0.0185795878987759,
0.0537605781840501));
#18019=CARTESIAN_POINT('Ctrl Pts',(0.0856431484406112,-0.159474177462153,
0.0460006022750521));
#18020=CARTESIAN_POINT('Ctrl Pts',(-0.0839657292871194,-0.160363143120653,
0.0382406263660544));
#18021=CARTESIAN_POINT('Ctrl Pts',(-0.179844832231877,-0.0204718628801216,
0.0304806504570563));
#18022=CARTESIAN_POINT('Ctrl Pts',(-0.117866479118068,0.137399078213474,
0.0227206745480585));
#18023=CARTESIAN_POINT('Ctrl Pts',(0.0476444145610997,0.174632482457551,
0.0149606986390605));
#18024=CARTESIAN_POINT('Ctrl Pts',(0.171219786572432,0.0585809927800803,
0.00720072273006264));
#18025=CARTESIAN_POINT('Ctrl Pts',(0.144688050375066,-0.108949473877577,
-0.000559253178935319));
#18026=CARTESIAN_POINT('Ctrl Pts',(-0.0092814439579932,-0.180735423716049,
-0.00831922908793317));
#18027=CARTESIAN_POINT('Ctrl Pts',(-0.105867686800049,-0.122947365648507,
-0.0134925463605985));
#18028=CARTESIAN_POINT('Ctrl Pts',(-0.131895903200816,-0.0800747195988904,
-0.0160792049969312));
#18029=CARTESIAN_POINT('Ctrl Pts',(-0.0374537582415196,-0.140096572423086,
0.245359734998977));
#18030=CARTESIAN_POINT('Ctrl Pts',(-0.0829920245295529,-0.127922261611689,
0.242773076362644));
#18031=CARTESIAN_POINT('Ctrl Pts',(-0.160591096949962,-0.0560317985556137,
0.237599759089979));
#18032=CARTESIAN_POINT('Ctrl Pts',(-0.13643521822445,0.101791299158848,
0.229839783180981));
#18033=CARTESIAN_POINT('Ctrl Pts',(0.00769506740980954,0.1699022237233,
0.222079807271983));
#18034=CARTESIAN_POINT('Ctrl Pts',(0.144969579481095,0.0890291096113304,
0.214319831362985));
#18035=CARTESIAN_POINT('Ctrl Pts',(0.155026424317845,-0.0700939445729984,
0.206559855453987));
#18036=CARTESIAN_POINT('Ctrl Pts',(0.0289569648011409,-0.167633527556011,
0.19879987954499));
#18037=CARTESIAN_POINT('Ctrl Pts',(-0.122519659046519,-0.118031231043151,
0.191039903635991));
#18038=CARTESIAN_POINT('Ctrl Pts',(-0.166442869216287,0.0352046776440443,
0.183279927726994));
#18039=CARTESIAN_POINT('Ctrl Pts',(-0.064240621638164,0.157527260611955,
0.175519951817996));
#18040=CARTESIAN_POINT('Ctrl Pts',(0.0943568867767351,0.141559037340679,
0.167759975908998));
#18041=CARTESIAN_POINT('Ctrl Pts',(0.170118841887737,0.00131313836865665,
0.16));
#18042=CARTESIAN_POINT('Ctrl Pts',(0.0965315639882279,-0.140084581027326,
0.152240024091002));
#18043=CARTESIAN_POINT('Ctrl Pts',(-0.0618012237018238,-0.158501476380598,
0.144480048182004));
#18044=CARTESIAN_POINT('Ctrl Pts',(-0.165878396703103,-0.0377684145673052,
0.136720072273006));
#18045=CARTESIAN_POINT('Ctrl Pts',(-0.124329541933827,0.116121687534276,
0.128960096364008));
#18046=CARTESIAN_POINT('Ctrl Pts',(0.0263691315170036,0.168067732987372,
0.12120012045501));
#18047=CARTESIAN_POINT('Ctrl Pts',(0.153918185014798,0.0724657594331675,
0.113440144546012));
#18048=CARTESIAN_POINT('Ctrl Pts',(0.146341206869619,-0.0867544378416841,
0.105680168637015));
#18049=CARTESIAN_POINT('Ctrl Pts',(0.0102902328814698,-0.169812269106107,
0.0979201927280167));
#18050=CARTESIAN_POINT('Ctrl Pts',(-0.134794781526993,-0.103790539737311,
0.0901602168190187));
#18051=CARTESIAN_POINT('Ctrl Pts',(-0.161542096774173,0.0533496359633175,
0.0824002409100209));
#18052=CARTESIAN_POINT('Ctrl Pts',(-0.0464709316213242,0.163653894581969,
0.074640265001023));
#18053=CARTESIAN_POINT('Ctrl Pts',(0.109398542213106,0.130284849835523,
0.066880289092025));
#18054=CARTESIAN_POINT('Ctrl Pts',(0.16922405906302,-0.0174617621848401,
0.0591203131830272));
#18055=CARTESIAN_POINT('Ctrl Pts',(0.0804904984426183,-0.149879543972585,
0.0513603372740291));
#18056=CARTESIAN_POINT('Ctrl Pts',(-0.0789139998409189,-0.150715025739123,
0.0436003613650314));
#18057=CARTESIAN_POINT('Ctrl Pts',(-0.169024614954586,-0.0192401899891918,
0.0358403854560333));
#18058=CARTESIAN_POINT('Ctrl Pts',(-0.110775138777956,0.12913257502003,
0.0280804095470356));
#18059=CARTESIAN_POINT('Ctrl Pts',(0.0447779273164969,0.164125861942445,
0.0203204336380375));
#18060=CARTESIAN_POINT('Ctrl Pts',(0.16091848811479,0.0550565152494576,
0.0125604577290397));
#18061=CARTESIAN_POINT('Ctrl Pts',(0.135983012131502,-0.10239461786658,
0.00480048182004171));
#18062=CARTESIAN_POINT('Ctrl Pts',(-0.00872303347143,-0.169861624730324,
-0.00295949408895612));
#18063=CARTESIAN_POINT('Ctrl Pts',(-0.0994982439886826,-0.115550337924785,
-0.00813281136162148));
#18064=CARTESIAN_POINT('Ctrl Pts',(-0.123960494032221,-0.0752570895690155,
-0.0107194699979541));
#18065=CARTESIAN_POINT('Ctrl Pts',(-0.0350561322973148,-0.13112820202432,
0.250719469997954));
#18066=CARTESIAN_POINT('Ctrl Pts',(-0.0776792377621743,-0.119733237394047,
0.248132811361621));
#18067=CARTESIAN_POINT('Ctrl Pts',(-0.150310756644121,-0.0524448876493412,
0.242959494088956));
#18068=CARTESIAN_POINT('Ctrl Pts',(-0.127701231722781,0.0952750649752511,
0.235199518179958));
#18069=CARTESIAN_POINT('Ctrl Pts',(0.00720246281869772,0.159025825767447,
0.22743954227096));
#18070=CARTESIAN_POINT('Ctrl Pts',(0.135689260463629,0.08332985503674,0.219679566361962));
#18071=CARTESIAN_POINT('Ctrl Pts',(0.145102310038447,-0.0656068365248246,
0.211919590452964));
#18072=CARTESIAN_POINT('Ctrl Pts',(0.0271032664452926,-0.156902361615465,
0.204159614543967));
#18073=CARTESIAN_POINT('Ctrl Pts',(-0.114676485837817,-0.110475387382534,
0.196399638634969));
#18074=CARTESIAN_POINT('Ctrl Pts',(-0.155787924019933,0.0329510280120788,
0.188639662725971));
#18075=CARTESIAN_POINT('Ctrl Pts',(-0.0601282177475243,0.147443053720694,
0.180879686816973));
#18076=CARTESIAN_POINT('Ctrl Pts',(0.0883165711883383,0.132497046328295,
0.173119710907975));
#18077=CARTESIAN_POINT('Ctrl Pts',(0.159228576983534,0.00122907698820117,
0.165359734998977));
#18078=CARTESIAN_POINT('Ctrl Pts',(0.0903520350672485,-0.131116978265319,
0.157599759089979));
#18079=CARTESIAN_POINT('Ctrl Pts',(-0.0578449794078444,-0.148354904452775,
0.149839783180981));
#18080=CARTESIAN_POINT('Ctrl Pts',(-0.155259586570517,-0.0353506457000499,
0.142079807271983));
#18081=CARTESIAN_POINT('Ctrl Pts',(-0.116370507931168,0.108688084505131,
0.134319831362985));
#18082=CARTESIAN_POINT('Ctrl Pts',(0.0246810949401768,0.157308771112418,
0.126559855453988));
#18083=CARTESIAN_POINT('Ctrl Pts',(0.144065015373005,0.0678268181615582,
0.118799879544989));
#18084=CARTESIAN_POINT('Ctrl Pts',(0.13697308226022,-0.0812007978143519,
0.111039903635992));
#18085=CARTESIAN_POINT('Ctrl Pts',(0.00963149713673027,-0.15894162965178,
0.103279927726994));
#18086=CARTESIAN_POINT('Ctrl Pts',(-0.126165808614623,-0.0971463229077874,
0.0955199518179957));
#18087=CARTESIAN_POINT('Ctrl Pts',(-0.151200877615086,0.0499344253861922,
0.087759975908998));
#18088=CARTESIAN_POINT('Ctrl Pts',(-0.0434960656388994,0.153177487354966,
0.08));
#18089=CARTESIAN_POINT('Ctrl Pts',(0.102395325569881,0.121944583043386,
0.072240024091002));
#18090=CARTESIAN_POINT('Ctrl Pts',(0.158391074245402,-0.0163439364709043,
0.0644800481820042));
#18091=CARTESIAN_POINT('Ctrl Pts',(0.0753378484446251,-0.140284910483017,
0.0567200722730062));
#18092=CARTESIAN_POINT('Ctrl Pts',(-0.0738622703947183,-0.141066908357593,
0.0489600963640083));
#18093=CARTESIAN_POINT('Ctrl Pts',(-0.158204397677296,-0.018008517098262,
0.0412001204550104));
#18094=CARTESIAN_POINT('Ctrl Pts',(-0.103683798437843,0.120866071826586,
0.0334401445460125));
#18095=CARTESIAN_POINT('Ctrl Pts',(0.0419114400718942,0.153619241427338,
0.0256801686370146));
#18096=CARTESIAN_POINT('Ctrl Pts',(0.150617189657149,0.051532037718835,
0.0179201927280167));
#18097=CARTESIAN_POINT('Ctrl Pts',(0.127277973887939,-0.0958397618555833,
0.0101602168190187));
#18098=CARTESIAN_POINT('Ctrl Pts',(-0.00816462298486686,-0.1589878257446,
0.00240024091002091));
#18099=CARTESIAN_POINT('Ctrl Pts',(-0.0931288011773165,-0.108153310201063,
-0.00277307636264444));
#18100=CARTESIAN_POINT('Ctrl Pts',(-0.116025084863626,-0.0704394595391406,
-0.00535973499897709));
#18101=CARTESIAN_POINT('Ctrl Pts',(-0.0326585063531099,-0.122159831625555,
0.256079204996931));
#18102=CARTESIAN_POINT('Ctrl Pts',(-0.0723664509947957,-0.111544213176404,
0.253492546360598));
#18103=CARTESIAN_POINT('Ctrl Pts',(-0.140030416338279,-0.0488579767430688,
0.248319229087933));
#18104=CARTESIAN_POINT('Ctrl Pts',(-0.118967245221113,0.0887588307916541,
0.240559253178936));
#18105=CARTESIAN_POINT('Ctrl Pts',(0.00670985822758596,0.148149427811594,
0.232799277269937));
#18106=CARTESIAN_POINT('Ctrl Pts',(0.126408941446163,0.0776306004621497,
0.225039301360939));
#18107=CARTESIAN_POINT('Ctrl Pts',(0.13517819575905,-0.0611197284766509,
0.217279325451942));
#18108=CARTESIAN_POINT('Ctrl Pts',(0.0252495680894444,-0.146171195674918,
0.209519349542944));
#18109=CARTESIAN_POINT('Ctrl Pts',(-0.106833312629116,-0.102919543721916,
0.201759373633946));
#18110=CARTESIAN_POINT('Ctrl Pts',(-0.14513297882358,0.0306973783801131,
0.193999397724948));
#18111=CARTESIAN_POINT('Ctrl Pts',(-0.0560158138568844,0.137358846829434,
0.18623942181595));
#18112=CARTESIAN_POINT('Ctrl Pts',(0.0822762555999414,0.12343505531591,
0.178479445906952));
#18113=CARTESIAN_POINT('Ctrl Pts',(0.148338312079331,0.00114501560774606,
0.170719469997954));
#18114=CARTESIAN_POINT('Ctrl Pts',(0.0841725061462688,-0.122149375503312,
0.162959494088956));
#18115=CARTESIAN_POINT('Ctrl Pts',(-0.0538887351138648,-0.138208332524951,
0.155199518179959));
#18116=CARTESIAN_POINT('Ctrl Pts',(-0.144640776437932,-0.0329328768327946,
0.14743954227096));
#18117=CARTESIAN_POINT('Ctrl Pts',(-0.108411473928508,0.101254481475986,
0.139679566361963));
#18118=CARTESIAN_POINT('Ctrl Pts',(0.0229930583633497,0.146549809237466,
0.131919590452964));
#18119=CARTESIAN_POINT('Ctrl Pts',(0.134211845731212,0.0631878768899486,
0.124159614543967));
#18120=CARTESIAN_POINT('Ctrl Pts',(0.127604957650822,-0.0756471577870196,
0.116399638634969));
#18121=CARTESIAN_POINT('Ctrl Pts',(0.00897276139199077,-0.148070990197453,
0.108639662725971));
#18122=CARTESIAN_POINT('Ctrl Pts',(-0.117536835702253,-0.0905021060782641,
0.100879686816973));
#18123=CARTESIAN_POINT('Ctrl Pts',(-0.140859658455999,0.0465192148090667,
0.0931197109079749));
#18124=CARTESIAN_POINT('Ctrl Pts',(-0.0405211996564747,0.142701080127962,
0.0853597349989771));
#18125=CARTESIAN_POINT('Ctrl Pts',(0.0953921089266558,0.113604316251249,
0.077599759089979));
#18126=CARTESIAN_POINT('Ctrl Pts',(0.147558089427783,-0.0152261107569683,
0.0698397831809813));
#18127=CARTESIAN_POINT('Ctrl Pts',(0.070185198446632,-0.130690276993449,
0.0620798072719832));
#18128=CARTESIAN_POINT('Ctrl Pts',(-0.0688105409485176,-0.131418790976063,
0.0543198313629854));
#18129=CARTESIAN_POINT('Ctrl Pts',(-0.147384180400005,-0.0167768442073323,
0.0465598554539874));
#18130=CARTESIAN_POINT('Ctrl Pts',(-0.0965924580977301,0.112599568633142,
0.0387998795449896));
#18131=CARTESIAN_POINT('Ctrl Pts',(0.0390449528272914,0.143112620912232,
0.0310399036359916));
#18132=CARTESIAN_POINT('Ctrl Pts',(0.140315891199508,0.0480075601882123,
0.0232799277269937));
#18133=CARTESIAN_POINT('Ctrl Pts',(0.118572935644375,-0.0892849058445864,
0.0155199518179958));
#18134=CARTESIAN_POINT('Ctrl Pts',(-0.00760621249830358,-0.148114026758875,
0.00775997590899793));
#18135=CARTESIAN_POINT('Ctrl Pts',(-0.0867593583659504,-0.100756282477341,
0.00258665863633259));
#18136=CARTESIAN_POINT('Ctrl Pts',(-0.108089675695031,-0.0656218295092657,
-5.55111512312578E-17));
#18137=CARTESIAN_POINT('Ctrl Pts',(-0.108089675695031,-0.0656218295092657,
-5.55111512312578E-17));
#18138=CARTESIAN_POINT('Ctrl Pts',(-0.104219465379748,-0.0739058869203245,
-4.02841154597017E-17));
#18139=CARTESIAN_POINT('Ctrl Pts',(-0.0994141168358061,-0.0816768736924768,
-5.16144647363644E-17));
#18140=CARTESIAN_POINT('Ctrl Pts',(-0.0938412360364922,-0.088871564406415,
-3.81639164714898E-17));
#18141=CARTESIAN_POINT('Ctrl Pts',(-0.0894001862863345,-0.094605040600905,
-2.74451237748006E-17));
#18142=CARTESIAN_POINT('Ctrl Pts',(-0.0844703330957707,-0.0999727304469881,
3.12377098840079E-17));
#18143=CARTESIAN_POINT('Ctrl Pts',(-0.0791158513129458,-0.104935071387697,
-1.21430643318376E-17));
#18144=CARTESIAN_POINT('Ctrl Pts',(-0.0766900604813501,-0.107183206995485,
-3.17962611543325E-17));
#18145=CARTESIAN_POINT('Ctrl Pts',(-0.0741829996358932,-0.109342173006691,
4.83248416902999E-17));
#18146=CARTESIAN_POINT('Ctrl Pts',(-0.0716059924168524,-0.111405381598006,
5.3776427755281E-17));
#18147=CARTESIAN_POINT('Ctrl Pts',(-0.0639212992135713,-0.117557915794061,
7.00331794132204E-17));
#18148=CARTESIAN_POINT('Ctrl Pts',(-0.0556061968393146,-0.12287204611112,
-5.69073736333764E-18));
#18149=CARTESIAN_POINT('Ctrl Pts',(-0.0468203466856493,-0.127256781127915,
5.55111512312578E-17));
#18150=CARTESIAN_POINT('Ctrl Pts',(-0.0434613267337519,-0.12893315986732,
7.89099528597243E-17));
#18151=CARTESIAN_POINT('Ctrl Pts',(-0.0400330653128497,-0.130473352587733,
3.97002991909352E-17));
#18152=CARTESIAN_POINT('Ctrl Pts',(-0.0365431560942257,-0.131870761756357,
6.59194920871187E-17));
#18153=CARTESIAN_POINT('Ctrl Pts',(-0.0339571636773035,-0.13290622981212,
8.5347686277821E-17));
#18154=CARTESIAN_POINT('Ctrl Pts',(-0.0313383144727484,-0.133862652235137,
-2.74403076010104E-17));
#18155=CARTESIAN_POINT('Ctrl Pts',(-0.0286994266230122,-0.134734580282325,
-2.42861286636753E-17));
#18156=CARTESIAN_POINT('Ctrl Pts',(-0.0216199050576346,-0.137073760181214,
-1.58242011095522E-17));
#18157=CARTESIAN_POINT('Ctrl Pts',(-0.0143790427459088,-0.138813119073991,
5.80198461902811E-17));
#18158=CARTESIAN_POINT('Ctrl Pts',(-0.0070411538297537,-0.139912507657099,
6.93889390390723E-17));
#18159=CARTESIAN_POINT('Ctrl Pts',(5.47883476400097E-5,-0.140975646920361,
8.02325614020808E-17));
#18160=CARTESIAN_POINT('Ctrl Pts',(0.00724182591717642,-0.141440539972256,
1.32011341321413E-16));
#18161=CARTESIAN_POINT('Ctrl Pts',(0.0144605478337719,-0.141339082434075,
1.61329283265843E-16));
#18162=CARTESIAN_POINT('Ctrl Pts',(0.0178811722145177,-0.141291006315792,
1.75221724083914E-16));
#18163=CARTESIAN_POINT('Ctrl Pts',(0.021310106848269,-0.141115105569205,
1.85534911235541E-16));
#18164=CARTESIAN_POINT('Ctrl Pts',(0.0247235715439624,-0.140816220288761,
1.71737624121704E-16));
#18165=CARTESIAN_POINT('Ctrl Pts',(0.0339754553361668,-0.140006119078294,
1.34341339582434E-16));
#18166=CARTESIAN_POINT('Ctrl Pts',(0.0431421008898472,-0.138295657968001,
8.04496487960062E-17));
#18167=CARTESIAN_POINT('Ctrl Pts',(0.0520992976556894,-0.135759125106636,
3.20923843055709E-17));
#18168=CARTESIAN_POINT('Ctrl Pts',(0.0590658916121619,-0.13378629867842,
-5.518202506064E-18));
#18169=CARTESIAN_POINT('Ctrl Pts',(0.0659062642374416,-0.131312982137409,
7.87850579480063E-17));
#18170=CARTESIAN_POINT('Ctrl Pts',(0.0725619642951071,-0.128359965266718,
7.63278329429795E-17));
#18171=CARTESIAN_POINT('Ctrl Pts',(0.0758074813473741,-0.126919986522721,
7.51296170399226E-17));
#18172=CARTESIAN_POINT('Ctrl Pts',(0.0790005264283722,-0.125369490597537,
8.38688896655138E-17));
#18173=CARTESIAN_POINT('Ctrl Pts',(0.0821329715644795,-0.123712761836801,
7.24247051220317E-17));
#18174=CARTESIAN_POINT('Ctrl Pts',(0.0888257654942848,-0.120172989003949,
4.79730178566093E-17));
#18175=CARTESIAN_POINT('Ctrl Pts',(0.0952446087626691,-0.116147988031934,
8.96774285244103E-17));
#18176=CARTESIAN_POINT('Ctrl Pts',(0.101324221742587,-0.111663228753314,
8.28330459778925E-17));
#18177=CARTESIAN_POINT('Ctrl Pts',(0.104638321741973,-0.109218510516871,
7.91020571356516E-17));
#18178=CARTESIAN_POINT('Ctrl Pts',(0.107849695272814,-0.106637925639498,
3.17151869302413E-17));
#18179=CARTESIAN_POINT('Ctrl Pts',(0.110939265073957,-0.10393289123317,
1.53956708492942E-17));
#18180=CARTESIAN_POINT('Ctrl Pts',(0.115072333360666,-0.100314234708527,
-6.43574216607592E-18));
#18181=CARTESIAN_POINT('Ctrl Pts',(0.118992075260627,-0.0964697210975667,
5.54296751400654E-17));
#18182=CARTESIAN_POINT('Ctrl Pts',(0.122673447199167,-0.0924082746861152,
3.52365706057789E-17));
#18183=CARTESIAN_POINT('Ctrl Pts',(0.125092164655522,-0.0897398425098966,
2.31620156359627E-17));
#18184=CARTESIAN_POINT('Ctrl Pts',(0.127407959881093,-0.0869777021544565,
-4.01489640485901E-17));
#18185=CARTESIAN_POINT('Ctrl Pts',(0.129620323775263,-0.0841289546921697,
-3.98986399474666E-17));
#18186=CARTESIAN_POINT('Ctrl Pts',(-0.126471935391749,0.000101176582396995,
0.195658032638058));
#18187=CARTESIAN_POINT('Ctrl Pts',(-0.126547267107008,0.00888033934128026,
0.195105154333688));
#18188=CARTESIAN_POINT('Ctrl Pts',(-0.125707148272093,0.0176451944231377,
0.194552276029318));
#18189=CARTESIAN_POINT('Ctrl Pts',(-0.12389684029672,0.0262048027713284,
0.193999397724948));
#18190=CARTESIAN_POINT('Ctrl Pts',(-0.115427257168015,0.0662512011965534,
0.191412739088615));
#18191=CARTESIAN_POINT('Ctrl Pts',(-0.0857215355124495,0.101805024012994,
0.188826080452282));
#18192=CARTESIAN_POINT('Ctrl Pts',(-0.0478199964418627,0.117261303502293,
0.18623942181595));
#18193=CARTESIAN_POINT('Ctrl Pts',(-0.0099184573712758,0.132717582991593,
0.183652763179617));
#18194=CARTESIAN_POINT('Ctrl Pts',(0.0361788991143328,0.128076319153751,
0.181066104543285));
#18195=CARTESIAN_POINT('Ctrl Pts',(0.070237920103702,0.105374013950137,
0.178479445906952));
#18196=CARTESIAN_POINT('Ctrl Pts',(0.104296941093071,0.0826717087465222,
0.175892787270619));
#18197=CARTESIAN_POINT('Ctrl Pts',(0.126317626586201,0.0419083621771342,
0.173306128634287));
#18198=CARTESIAN_POINT('Ctrl Pts',(0.126633668343922,0.000977623707263797,
0.170719469997954));
#18199=CARTESIAN_POINT('Ctrl Pts',(0.126949710101644,-0.0399531147626067,
0.168132811361621));
#18200=CARTESIAN_POINT('Ctrl Pts',(0.105561108123956,-0.08105124513296,
0.165546152725289));
#18201=CARTESIAN_POINT('Ctrl Pts',(0.0718566002584231,-0.104276803155076,
0.162959494088956));
#18202=CARTESIAN_POINT('Ctrl Pts',(0.0381520923928904,-0.127502361177192,
0.160372835452623));
#18203=CARTESIAN_POINT('Ctrl Pts',(-0.00786832136048696,-0.132855346851071,
0.157786176816291));
#18204=CARTESIAN_POINT('Ctrl Pts',(-0.0460038684578537,-0.117985930405985,
0.155199518179958));
#18205=CARTESIAN_POINT('Ctrl Pts',(-0.0841394155552204,-0.103116513960899,
0.152612859543626));
#18206=CARTESIAN_POINT('Ctrl Pts',(-0.114390095996576,-0.0680246953968468,
0.150026200907293));
#18207=CARTESIAN_POINT('Ctrl Pts',(-0.12347721913235,-0.0281142263966907,
0.14743954227096));
#18208=CARTESIAN_POINT('Ctrl Pts',(-0.125563410841138,-0.018951712774069,
0.14684570572666));
#18209=CARTESIAN_POINT('Ctrl Pts',(-0.126534167537385,-0.00953522996602069,
0.146251869182359));
#18210=CARTESIAN_POINT('Ctrl Pts',(-0.126453631260982,-0.000102348163238207,
0.145658032638058));
#18211=CARTESIAN_POINT('Ctrl Pts',(-0.0398513841857245,-0.149064942821851,
0.24));
#18212=CARTESIAN_POINT('Ctrl Pts',(-0.0498806325786677,-0.145400296738327,
0.24));
#18213=CARTESIAN_POINT('Ctrl Pts',(-0.0594363948008725,-0.140639648297949,
0.24));
#18214=CARTESIAN_POINT('Ctrl Pts',(-0.0684062055177017,-0.134931499399492,
0.24));
#18215=CARTESIAN_POINT('Ctrl Pts',(-0.0735915624001909,-0.131631676235849,
0.24));
#18216=CARTESIAN_POINT('Ctrl Pts',(-0.0785806353345173,-0.128014298080738,
0.24));
#18217=CARTESIAN_POINT('Ctrl Pts',(-0.0833462611484583,-0.124102693747304,
0.24));
#18218=CARTESIAN_POINT('Ctrl Pts',(-0.0858656342542594,-0.122034803580736,
0.24));
#18219=CARTESIAN_POINT('Ctrl Pts',(-0.0883241156266364,-0.11988309220465,
0.24));
#18220=CARTESIAN_POINT('Ctrl Pts',(-0.0907117892851122,-0.117655751751618,
0.24));
#18221=CARTESIAN_POINT('Ctrl Pts',(-0.0983819858496404,-0.110500611839494,
0.24));
#18222=CARTESIAN_POINT('Ctrl Pts',(-0.105284458416918,-0.102606966330569,
0.24));
#18223=CARTESIAN_POINT('Ctrl Pts',(-0.111294422020379,-0.0941015332659665,
0.24));
#18224=CARTESIAN_POINT('Ctrl Pts',(-0.114410577497229,-0.0896914812962706,
0.24));
#18225=CARTESIAN_POINT('Ctrl Pts',(-0.117286101138547,-0.0851164738413172,
0.24));
#18226=CARTESIAN_POINT('Ctrl Pts',(-0.119898298320422,-0.0803922539627851,
0.24));
#18227=CARTESIAN_POINT('Ctrl Pts',(-0.1222721977331,-0.0760990011896685,
0.24));
#18228=CARTESIAN_POINT('Ctrl Pts',(-0.124430744329062,-0.0716759619599862,
0.24));
#18229=CARTESIAN_POINT('Ctrl Pts',(-0.126341093034125,-0.0671690272221462,
0.24));
#18230=CARTESIAN_POINT('Ctrl Pts',(-0.129206708925078,-0.060408406100978,
0.24));
#18231=CARTESIAN_POINT('Ctrl Pts',(-0.131522065955468,-0.0534490321795157,
0.24));
#18232=CARTESIAN_POINT('Ctrl Pts',(-0.133233091500091,-0.0463330844490581,
0.24));
#18233=CARTESIAN_POINT('Ctrl Pts',(-0.135004134506116,-0.0389675313754268,
0.24));
#18234=CARTESIAN_POINT('Ctrl Pts',(-0.136127599829873,-0.0314337185245799,
0.24));
#18235=CARTESIAN_POINT('Ctrl Pts',(-0.136615064298196,-0.0238138180582873,
0.24));
#18236=CARTESIAN_POINT('Ctrl Pts',(-0.136813484749433,-0.0207121682209076,
0.24));
#18237=CARTESIAN_POINT('Ctrl Pts',(-0.136906013213758,-0.0175970392000076,
0.24));
#18238=CARTESIAN_POINT('Ctrl Pts',(-0.136893785357156,-0.0144871321155608,
0.24));
#18239=CARTESIAN_POINT('Ctrl Pts',(-0.136861203984761,-0.00620072149302863,
0.24));
#18240=CARTESIAN_POINT('Ctrl Pts',(-0.136088646936857,0.00207357465703332,
0.24));
#18241=CARTESIAN_POINT('Ctrl Pts',(-0.134599584032292,0.0102285531249486,
0.24));
#18242=CARTESIAN_POINT('Ctrl Pts',(-0.133676409755049,0.0152843948425598,
0.24));
#18243=CARTESIAN_POINT('Ctrl Pts',(-0.132477333465274,0.0202942984003417,
0.24));
#18244=CARTESIAN_POINT('Ctrl Pts',(-0.131003622030167,0.0252303138624672,
0.24));
#18245=CARTESIAN_POINT('Ctrl Pts',(-0.129740734874544,0.029460199292259,
0.24));
#18246=CARTESIAN_POINT('Ctrl Pts',(-0.128274507607502,0.0336384499732856,
0.24));
#18247=CARTESIAN_POINT('Ctrl Pts',(-0.126614574688298,0.0377237273426867,
0.24));
#18248=CARTESIAN_POINT('Ctrl Pts',(-0.124573382985647,0.042747324485064,
0.24));
#18249=CARTESIAN_POINT('Ctrl Pts',(-0.122237651925267,0.0476379767326878,
0.24));
#18250=CARTESIAN_POINT('Ctrl Pts',(-0.119609691052418,0.0523617558795304,
0.24));
#18251=CARTESIAN_POINT('Ctrl Pts',(-0.117006563775536,0.0570408964535612,
0.24));
#18252=CARTESIAN_POINT('Ctrl Pts',(-0.114113358229268,0.0615597689541448,
0.24));
#18253=CARTESIAN_POINT('Ctrl Pts',(-0.110947628485839,0.0658586917144141,
0.24));
#18254=CARTESIAN_POINT('Ctrl Pts',(-0.108265305855902,0.0695011687224882,
0.24));
#18255=CARTESIAN_POINT('Ctrl Pts',(-0.105385772272888,0.0729892759232728,
0.24));
#18256=CARTESIAN_POINT('Ctrl Pts',(-0.102309360287629,0.0763011815833395,
0.24));
#18257=CARTESIAN_POINT('Ctrl Pts',(-0.100282916666232,0.0784827457339379,
0.24));
#18258=CARTESIAN_POINT('Ctrl Pts',(-0.0981709975111385,0.0805877996091198,
0.24));
#18259=CARTESIAN_POINT('Ctrl Pts',(-0.0959791030802606,0.0826138105732947,
0.24));
#18260=CARTESIAN_POINT('Origin',(0.,0.,0.24));
#18261=CARTESIAN_POINT('',(0.158771324027147,-0.275,0.24));
#18262=CARTESIAN_POINT('',(0.317542648054294,0.,0.24));
#18263=CARTESIAN_POINT('',(0.158771324027147,-0.275,0.24));
#18264=CARTESIAN_POINT('',(0.158771324027147,0.275,0.24));
#18265=CARTESIAN_POINT('',(0.317542648054294,0.,0.24));
#18266=CARTESIAN_POINT('',(-0.158771324027147,0.275,0.24));
#18267=CARTESIAN_POINT('',(0.158771324027147,0.275,0.24));
#18268=CARTESIAN_POINT('',(-0.317542648054294,5.55111512312578E-17,0.24));
#18269=CARTESIAN_POINT('',(-0.158771324027147,0.275,0.24));
#18270=CARTESIAN_POINT('',(-0.158771324027147,-0.275,0.24));
#18271=CARTESIAN_POINT('',(-0.317542648054294,3.88877587532466E-17,0.24));
#18272=CARTESIAN_POINT('',(-0.158771324027147,-0.275,0.24));
#18273=CARTESIAN_POINT('Origin',(0.,0.,0.12));
#18274=CARTESIAN_POINT('Origin',(-0.158771324027147,-0.275,0.));
#18275=CARTESIAN_POINT('',(-0.158771324027147,-0.275,0.));
#18276=CARTESIAN_POINT('',(0.158771324027147,-0.275,0.));
#18277=CARTESIAN_POINT('',(-0.158771324027147,-0.275,0.));
#18278=CARTESIAN_POINT('',(0.158771324027147,-0.275,0.));
#18279=CARTESIAN_POINT('',(-0.158771324027147,-0.275,0.));
#18280=CARTESIAN_POINT('Origin',(-0.317542648054294,3.88877587532466E-17,
0.));
#18281=CARTESIAN_POINT('',(-0.317542648054294,3.88877587532466E-17,0.));
#18282=CARTESIAN_POINT('',(-0.317542648054294,3.88877587532466E-17,0.));
#18283=CARTESIAN_POINT('',(-0.317542648054294,3.88877587532466E-17,0.));
#18284=CARTESIAN_POINT('Origin',(-0.158771324027147,0.275,0.));
#18285=CARTESIAN_POINT('',(-0.158771324027147,0.275,0.));
#18286=CARTESIAN_POINT('',(-0.158771324027147,0.275,0.));
#18287=CARTESIAN_POINT('',(-0.158771324027147,0.275,0.));
#18288=CARTESIAN_POINT('Origin',(0.158771324027147,0.275,0.));
#18289=CARTESIAN_POINT('',(0.158771324027147,0.275,0.));
#18290=CARTESIAN_POINT('',(0.158771324027147,0.275,0.));
#18291=CARTESIAN_POINT('',(0.158771324027147,0.275,0.));
#18292=CARTESIAN_POINT('Origin',(0.317542648054294,0.,0.));
#18293=CARTESIAN_POINT('',(0.317542648054294,0.,0.));
#18294=CARTESIAN_POINT('',(0.317542648054294,0.,0.));
#18295=CARTESIAN_POINT('',(0.317542648054294,0.,0.));
#18296=CARTESIAN_POINT('Origin',(0.158771324027147,-0.275,0.));
#18297=CARTESIAN_POINT('',(0.158771324027147,-0.275,0.));
#18298=CARTESIAN_POINT('Origin',(0.,0.,0.));
#18339=UNCERTAINTY_MEASURE_WITH_UNIT(LENGTH_MEASURE(0.001),#18354,
'DISTANCE_ACCURACY_VALUE',
'Maximum model space distance between geometric entities at asserted c
onnectivities');
#18341=UNCERTAINTY_MEASURE_WITH_UNIT(LENGTH_MEASURE(0.001),#18354,
'DISTANCE_ACCURACY_VALUE',
'Maximum model space distance between geometric entities at asserted c
onnectivities');
#18351=(
GEOMETRIC_REPRESENTATION_CONTEXT(3)
GLOBAL_UNCERTAINTY_ASSIGNED_CONTEXT((#18339))
GLOBAL_UNIT_ASSIGNED_CONTEXT((#18354,#18356,#18357))
REPRESENTATION_CONTEXT('','3D')
);
#18353=(
GEOMETRIC_REPRESENTATION_CONTEXT(3)
GLOBAL_UNCERTAINTY_ASSIGNED_CONTEXT((#18341))
GLOBAL_UNIT_ASSIGNED_CONTEXT((#18354,#18356,#18357))
REPRESENTATION_CONTEXT('','3D')
);
#18354=(
LENGTH_UNIT()
NAMED_UNIT(*)
SI_UNIT(.CENTI.,.METRE.)
);
#18356=(
NAMED_UNIT(*)
PLANE_ANGLE_UNIT()
SI_UNIT($,.RADIAN.)
);
#18357=(
NAMED_UNIT(*)
SI_UNIT($,.STERADIAN.)
SOLID_ANGLE_UNIT()
);
#18367=SHAPE_DEFINITION_REPRESENTATION(#18378,#18405);
#18378=PRODUCT_DEFINITION_SHAPE('',$,#18417);
#18405=SHAPE_REPRESENTATION('',(#7031),#18351);
#18407=PRODUCT_DEFINITION_CONTEXT('part definition',#18442,'design');
#18417=PRODUCT_DEFINITION('2026-11-10-01-32-12-368','Hex nut M3',#18428,
#18407);
#18428=PRODUCT_DEFINITION_FORMATION('',$,#18453);
#18442=APPLICATION_CONTEXT(
'Core Data for Automotive Mechanical Design Process');
#18443=PRODUCT_CONTEXT('part definition',#18442,'mechanical');
#18453=PRODUCT('2026-11-10-01-32-12-368','Hex nut M3',$,(#18443));
#18461=PRESENTATION_STYLE_ASSIGNMENT((#18469));
#18469=SURFACE_STYLE_USAGE(.BOTH.,#18477);
#18477=SURFACE_SIDE_STYLE('',(#18485));
#18485=SURFACE_STYLE_FILL_AREA(#18493);
#18493=FILL_AREA_STYLE('Fastener gray',(#18501));
#18501=FILL_AREA_STYLE_COLOUR('Fastener gray',#18509);
#18509=COLOUR_RGB('Fastener gray',0.607843137254902,0.643137254901961,0.698039215686274);
ENDSEC;
END-ISO-10303-21;
